ISO-10303-21;
HEADER;
/* Generated by software containing ST-Developer
 * from STEP Tools, Inc. (www.steptools.com) 
 */

FILE_DESCRIPTION(
/* description */ ('Independent manual two-gate roller-track escapement for nominal30mm d
iameter20mm wide feed rollers. Opposed gates are driven by native capt
ured pin-slot loops with positive curved-slot travel stops at\X\B116de
g. Repeated gate/pin/washer/clip instances, adapted native common bear
ing families, full retaining lips and rotating polymer grip. External 
workpieces, gravity feeder/incline and mount anchors outside assembly.
 No powered-feed compatibility, impact, capacity, safety, force, wear 
or life rating.'),
/* implementation_level */ '2;1');

FILE_NAME(
/* name */ 'Shoulder screw M6x8.step',
/* time_stamp */ '2026-11-08T18:43:23-08:00',
/* author */ (''),
/* organization */ (''),
/* preprocessor_version */ 'ST-DEVELOPER v20.2',
/* originating_system */ 'Autodesk Translation Framework v15.17.0.0',
/* authorisation */ '');

FILE_SCHEMA (('AUTOMOTIVE_DESIGN { 1 0 10303 214 3 1 1 }'));
ENDSEC;

DATA;
#10=MECHANICAL_DESIGN_GEOMETRIC_PRESENTATION_REPRESENTATION('',(#472),#19863);
#115=CONICAL_SURFACE('',#7094,2.5,0.785398163397448);
#123=B_SPLINE_SURFACE_WITH_KNOTS('',3,3,((#16881,#16882,#16883,#16884,#16885,
#16886,#16887,#16888,#16889,#16890,#16891,#16892,#16893,#16894,#16895,#16896,
#16897,#16898,#16899,#16900,#16901,#16902,#16903,#16904,#16905,#16906,#16907,
#16908,#16909,#16910,#16911,#16912,#16913,#16914,#16915,#16916,#16917,#16918,
#16919,#16920,#16921,#16922,#16923,#16924,#16925,#16926,#16927,#16928,#16929,
#16930,#16931,#16932,#16933),(#16934,#16935,#16936,#16937,#16938,#16939,
#16940,#16941,#16942,#16943,#16944,#16945,#16946,#16947,#16948,#16949,#16950,
#16951,#16952,#16953,#16954,#16955,#16956,#16957,#16958,#16959,#16960,#16961,
#16962,#16963,#16964,#16965,#16966,#16967,#16968,#16969,#16970,#16971,#16972,
#16973,#16974,#16975,#16976,#16977,#16978,#16979,#16980,#16981,#16982,#16983,
#16984,#16985,#16986),(#16987,#16988,#16989,#16990,#16991,#16992,#16993,
#16994,#16995,#16996,#16997,#16998,#16999,#17000,#17001,#17002,#17003,#17004,
#17005,#17006,#17007,#17008,#17009,#17010,#17011,#17012,#17013,#17014,#17015,
#17016,#17017,#17018,#17019,#17020,#17021,#17022,#17023,#17024,#17025,#17026,
#17027,#17028,#17029,#17030,#17031,#17032,#17033,#17034,#17035,#17036,#17037,
#17038,#17039),(#17040,#17041,#17042,#17043,#17044,#17045,#17046,#17047,
#17048,#17049,#17050,#17051,#17052,#17053,#17054,#17055,#17056,#17057,#17058,
#17059,#17060,#17061,#17062,#17063,#17064,#17065,#17066,#17067,#17068,#17069,
#17070,#17071,#17072,#17073,#17074,#17075,#17076,#17077,#17078,#17079,#17080,
#17081,#17082,#17083,#17084,#17085,#17086,#17087,#17088,#17089,#17090,#17091,
#17092)),.UNSPECIFIED.,.F.,.F.,.F.,(4,4),(4,1,1,1,1,1,1,1,1,1,1,1,1,1,1,
1,1,1,1,1,1,1,1,1,1,1,1,1,1,1,1,1,1,1,1,1,1,1,1,1,1,1,1,1,1,1,1,1,1,1,4),
(0.,0.0658467982010768),(13.9508069857623,14.9507739156503,15.9507408455384,
16.9507077754264,17.9506747053144,18.9506416352025,19.9506085650905,20.9505754949786,
21.9505424248666,22.9505093547546,23.9504762846427,24.9504432145307,25.9504101444187,
26.9503770743068,27.9503440041948,28.9503109340829,29.9502778639709,30.9502447938589,
31.950211723747,32.950178653635,33.950145583523,34.9501125134111,35.9500794432991,
36.9500463731871,37.9500133030752,38.9499802329632,39.9499471628512,40.9499140927393,
41.9498810226273,42.9498479525154,43.9498148824034,44.9497818122914,45.9497487421795,
46.9497156720675,47.9496826019555,48.9496495318436,49.9496164617316,50.9495833916196,
51.9495503215077,52.9495172513957,53.9494841812838,54.9494511111718,55.9494180410598,
56.9493849709479,57.9493519008359,58.9493188307239,59.949285760612,60.9492526905,
61.949219620388,62.9491865502761,63.9491534801641),.UNSPECIFIED.);
#124=B_SPLINE_SURFACE_WITH_KNOTS('',3,3,((#17265,#17266,#17267,#17268,#17269,
#17270,#17271,#17272,#17273,#17274,#17275,#17276,#17277,#17278,#17279,#17280,
#17281,#17282,#17283,#17284,#17285,#17286,#17287,#17288,#17289,#17290,#17291,
#17292,#17293,#17294,#17295,#17296,#17297,#17298,#17299,#17300,#17301,#17302,
#17303,#17304,#17305,#17306,#17307,#17308,#17309,#17310,#17311,#17312,#17313,
#17314,#17315),(#17316,#17317,#17318,#17319,#17320,#17321,#17322,#17323,
#17324,#17325,#17326,#17327,#17328,#17329,#17330,#17331,#17332,#17333,#17334,
#17335,#17336,#17337,#17338,#17339,#17340,#17341,#17342,#17343,#17344,#17345,
#17346,#17347,#17348,#17349,#17350,#17351,#17352,#17353,#17354,#17355,#17356,
#17357,#17358,#17359,#17360,#17361,#17362,#17363,#17364,#17365,#17366),
(#17367,#17368,#17369,#17370,#17371,#17372,#17373,#17374,#17375,#17376,
#17377,#17378,#17379,#17380,#17381,#17382,#17383,#17384,#17385,#17386,#17387,
#17388,#17389,#17390,#17391,#17392,#17393,#17394,#17395,#17396,#17397,#17398,
#17399,#17400,#17401,#17402,#17403,#17404,#17405,#17406,#17407,#17408,#17409,
#17410,#17411,#17412,#17413,#17414,#17415,#17416,#17417),(#17418,#17419,
#17420,#17421,#17422,#17423,#17424,#17425,#17426,#17427,#17428,#17429,#17430,
#17431,#17432,#17433,#17434,#17435,#17436,#17437,#17438,#17439,#17440,#17441,
#17442,#17443,#17444,#17445,#17446,#17447,#17448,#17449,#17450,#17451,#17452,
#17453,#17454,#17455,#17456,#17457,#17458,#17459,#17460,#17461,#17462,#17463,
#17464,#17465,#17466,#17467,#17468)),.UNSPECIFIED.,.F.,.F.,.F.,(4,4),(4,
1,1,1,1,1,1,1,1,1,1,1,1,1,1,1,1,1,1,1,1,1,1,1,1,1,1,1,1,1,1,1,1,1,1,1,1,
1,1,1,1,1,1,1,1,1,1,1,4),(0.,0.0658467982010768),(12.7118898652542,13.7104254552436,
14.7089610452331,15.7074966352225,16.7060322252119,17.7045678152014,18.7031034051908,
19.7016389951802,20.7001745851697,21.6987101751591,22.6972457651485,23.695781355138,
24.6943169451274,25.6928525351168,26.6913881251062,27.6899237150957,28.6884593050851,
29.6869948950745,30.685530485064,31.6840660750534,32.6826016650428,33.6811372550323,
34.6796728450217,35.6782084350111,36.6767440250006,37.67527961499,38.6738152049794,
39.6723507949688,40.6708863849583,41.6694219749477,42.6679575649371,43.6664931549266,
44.665028744916,45.6635643349054,46.6620999248949,47.6606355148843,48.6591711048737,
49.6577066948632,50.6562422848526,51.654777874842,52.6533134648314,53.6518490548209,
54.6503846448103,55.6489202347997,56.6474558247892,57.6459914147786,58.644527004768,
59.6430625947575,60.6415981847469),.UNSPECIFIED.);
#317=B_SPLINE_CURVE_WITH_KNOTS('',3,(#16050,#16051,#16052,#16053,#16054,
#16055),.UNSPECIFIED.,.F.,.F.,(4,1,1,4),(59.6902604182061,59.949285760612,
60.9492526905,61.880515305255),.UNSPECIFIED.);
#318=B_SPLINE_CURVE_WITH_KNOTS('',3,(#16058,#16059,#16060,#16061),
 .UNSPECIFIED.,.F.,.F.,(4,4),(59.6902604182061,60.6415981847469),
 .UNSPECIFIED.);
#319=B_SPLINE_CURVE_WITH_KNOTS('',3,(#16066,#16067,#16068,#16069,#16070,
#16071,#16072,#16073,#16074,#16075),.UNSPECIFIED.,.F.,.F.,(4,1,1,1,1,1,
1,4),(53.4070751110265,53.9494841812838,54.9494511111718,55.9494180410598,
56.9493849709479,57.9493519008359,58.9493188307239,59.6902604182061),
 .UNSPECIFIED.);
#320=B_SPLINE_CURVE_WITH_KNOTS('',3,(#16076,#16077,#16078,#16079,#16080,
#16081,#16082,#16083,#16084,#16085,#16086),.UNSPECIFIED.,.F.,.F.,(4,1,1,
1,1,1,1,1,4),(53.4070751110265,53.6518490548209,54.6503846448103,55.6489202347997,
56.6474558247892,57.6459914147786,58.644527004768,59.6430625947575,59.6902604182061),
 .UNSPECIFIED.);
#321=B_SPLINE_CURVE_WITH_KNOTS('',3,(#16091,#16092,#16093,#16094,#16095,
#16096,#16097,#16098,#16099,#16100),.UNSPECIFIED.,.F.,.F.,(4,1,1,1,1,1,
1,4),(47.1238898038469,47.9496826019555,48.9496495318436,49.9496164617316,
50.9495833916196,51.9495503215077,52.9495172513957,53.4070751110265),
 .UNSPECIFIED.);
#322=B_SPLINE_CURVE_WITH_KNOTS('',3,(#16101,#16102,#16103,#16104,#16105,
#16106,#16107,#16108,#16109,#16110),.UNSPECIFIED.,.F.,.F.,(4,1,1,1,1,1,
1,4),(47.1238898038469,47.6606355148843,48.6591711048737,49.6577066948632,
50.6562422848526,51.654777874842,52.6533134648314,53.4070751110265),
 .UNSPECIFIED.);
#323=B_SPLINE_CURVE_WITH_KNOTS('',3,(#16115,#16116,#16117,#16118,#16119,
#16120,#16121,#16122,#16123,#16124,#16125),.UNSPECIFIED.,.F.,.F.,(4,1,1,
1,1,1,1,1,4),(40.8407044966673,40.9499140927393,41.9498810226273,42.9498479525154,
43.9498148824034,44.9497818122914,45.9497487421795,46.9497156720675,47.1238898038469),
 .UNSPECIFIED.);
#324=B_SPLINE_CURVE_WITH_KNOTS('',3,(#16126,#16127,#16128,#16129,#16130,
#16131,#16132,#16133,#16134,#16135),.UNSPECIFIED.,.F.,.F.,(4,1,1,1,1,1,
1,4),(40.8407044966673,41.6694219749477,42.6679575649371,43.6664931549266,
44.665028744916,45.6635643349054,46.6620999248949,47.1238898038469),
 .UNSPECIFIED.);
#325=B_SPLINE_CURVE_WITH_KNOTS('',3,(#16140,#16141,#16142,#16143,#16144,
#16145,#16146,#16147,#16148,#16149),.UNSPECIFIED.,.F.,.F.,(4,1,1,1,1,1,
1,4),(34.5575191894877,34.9501125134111,35.9500794432991,36.9500463731871,
37.9500133030752,38.9499802329632,39.9499471628512,40.8407044966673),
 .UNSPECIFIED.);
#326=B_SPLINE_CURVE_WITH_KNOTS('',3,(#16150,#16151,#16152,#16153,#16154,
#16155,#16156,#16157,#16158,#16159,#16160),.UNSPECIFIED.,.F.,.F.,(4,1,1,
1,1,1,1,1,4),(34.5575191894877,34.6796728450217,35.6782084350111,36.6767440250006,
37.67527961499,38.6738152049794,39.6723507949688,40.6708863849583,40.8407044966673),
 .UNSPECIFIED.);
#327=B_SPLINE_CURVE_WITH_KNOTS('',3,(#16165,#16166,#16167,#16168,#16169,
#16170,#16171,#16172,#16173,#16174),.UNSPECIFIED.,.F.,.F.,(4,1,1,1,1,1,
1,4),(28.2743338823081,28.9503109340829,29.9502778639709,30.9502447938589,
31.950211723747,32.950178653635,33.950145583523,34.5575191894877),
 .UNSPECIFIED.);
#328=B_SPLINE_CURVE_WITH_KNOTS('',3,(#16175,#16176,#16177,#16178,#16179,
#16180,#16181,#16182,#16183,#16184),.UNSPECIFIED.,.F.,.F.,(4,1,1,1,1,1,
1,4),(28.2743338823081,28.6884593050851,29.6869948950745,30.685530485064,
31.6840660750534,32.6826016650428,33.6811372550323,34.5575191894877),
 .UNSPECIFIED.);
#329=B_SPLINE_CURVE_WITH_KNOTS('',3,(#16189,#16190,#16191,#16192,#16193,
#16194,#16195,#16196,#16197,#16198),.UNSPECIFIED.,.F.,.F.,(4,1,1,1,1,1,
1,4),(21.9911485751285,22.9505093547546,23.9504762846427,24.9504432145307,
25.9504101444187,26.9503770743068,27.9503440041948,28.2743338823081),
 .UNSPECIFIED.);
#330=B_SPLINE_CURVE_WITH_KNOTS('',3,(#16199,#16200,#16201,#16202,#16203,
#16204,#16205,#16206,#16207,#16208),.UNSPECIFIED.,.F.,.F.,(4,1,1,1,1,1,
1,4),(21.9911485751285,22.6972457651485,23.695781355138,24.6943169451274,
25.6928525351168,26.6913881251062,27.6899237150957,28.2743338823081),
 .UNSPECIFIED.);
#331=B_SPLINE_CURVE_WITH_KNOTS('',3,(#16213,#16214,#16215,#16216,#16217,
#16218,#16219,#16220,#16221,#16222,#16223),.UNSPECIFIED.,.F.,.F.,(4,1,1,
1,1,1,1,1,4),(15.707963267949,15.9507408455384,16.9507077754264,17.9506747053144,
18.9506416352025,19.9506085650905,20.9505754949786,21.9505424248666,21.9911485751285),
 .UNSPECIFIED.);
#332=B_SPLINE_CURVE_WITH_KNOTS('',3,(#16224,#16225,#16226,#16227,#16228,
#16229,#16230,#16231,#16232,#16233),.UNSPECIFIED.,.F.,.F.,(4,1,1,1,1,1,
1,4),(15.7079632679489,16.7060322252119,17.7045678152014,18.7031034051908,
19.7016389951802,20.7001745851697,21.6987101751591,21.9911485751285),
 .UNSPECIFIED.);
#333=B_SPLINE_CURVE_WITH_KNOTS('',3,(#16239,#16240,#16241,#16242,#16243,
#16244,#16245,#16246,#16247,#16248,#16249,#16250,#16251),.UNSPECIFIED.,
 .F.,.F.,(4,3,3,3,4),(-10.3761157273102,-10.3355095770483,-9.33554264716025,
-8.33557571727222,-7.9873987342723),.UNSPECIFIED.);
#334=B_SPLINE_CURVE_WITH_KNOTS('',3,(#16254,#16255,#16256,#16257,#16258,
#16259,#16260),.UNSPECIFIED.,.F.,.F.,(4,3,4),(5.91876055936317,6.401483492832,
7.40048571554784),.UNSPECIFIED.);
#335=B_SPLINE_CURVE_WITH_KNOTS('',3,(#16265,#16266,#16267,#16268,#16269,
#16270,#16271,#16272,#16273,#16274,#16275,#16276,#16277,#16278,#16279,#16280,
#16281,#16282,#16283,#16284,#16285,#16286),.UNSPECIFIED.,.F.,.F.,(4,3,3,
3,3,3,3,4),(-16.6593010344898,-16.3353111563765,-15.3353442264885,-14.3353772966004,
-13.3354103667124,-12.3354434368244,-11.3354765069363,-10.3761157273102),
 .UNSPECIFIED.);
#336=B_SPLINE_CURVE_WITH_KNOTS('',3,(#16287,#16288,#16289,#16290,#16291,
#16292,#16293,#16294,#16295,#16296,#16297,#16298,#16299,#16300,#16301,#16302,
#16303,#16304,#16305,#16306,#16307,#16308),.UNSPECIFIED.,.F.,.F.,(4,3,3,
3,3,3,3,4),(7.40048571554784,8.39855467281086,9.39709026280029,10.3956258527897,
11.3941614427792,12.3926970327686,13.391232622758,13.6836710227274),
 .UNSPECIFIED.);
#337=B_SPLINE_CURVE_WITH_KNOTS('',3,(#16313,#16314,#16315,#16316,#16317,
#16318,#16319,#16320,#16321,#16322,#16323,#16324,#16325,#16326,#16327,#16328,
#16329,#16330,#16331,#16332,#16333,#16334),.UNSPECIFIED.,.F.,.F.,(4,3,3,
3,3,3,3,4),(-22.9424863416694,-22.3351127357047,-21.3351458058167,-20.3351788759286,
-19.3352119460406,-18.3352450161526,-17.3352780862645,-16.6593010344898),
 .UNSPECIFIED.);
#338=B_SPLINE_CURVE_WITH_KNOTS('',3,(#16335,#16336,#16337,#16338,#16339,
#16340,#16341,#16342,#16343,#16344,#16345,#16346,#16347,#16348,#16349,#16350,
#16351,#16352,#16353,#16354,#16355,#16356),.UNSPECIFIED.,.F.,.F.,(4,3,3,
3,3,3,3,4),(13.6836710227274,14.3897682127475,15.3883038027369,16.3868393927263,
17.3853749827157,18.3839105727052,19.3824461626946,19.966856329907),
 .UNSPECIFIED.);
#339=B_SPLINE_CURVE_WITH_KNOTS('',3,(#16361,#16362,#16363,#16364,#16365,
#16366,#16367,#16368,#16369,#16370,#16371,#16372,#16373,#16374,#16375,#16376,
#16377,#16378,#16379,#16380,#16381,#16382),.UNSPECIFIED.,.F.,.F.,(4,3,3,
3,3,3,3,4),(-29.225671648849,-28.3349143150329,-27.3349473851449,-26.3349804552569,
-25.3350135253688,-24.3350465954808,-23.3350796655928,-22.9424863416694),
 .UNSPECIFIED.);
#340=B_SPLINE_CURVE_WITH_KNOTS('',3,(#16383,#16384,#16385,#16386,#16387,
#16388,#16389,#16390,#16391,#16392,#16393,#16394,#16395,#16396,#16397,#16398,
#16399,#16400,#16401,#16402,#16403,#16404),.UNSPECIFIED.,.F.,.F.,(4,3,3,
3,3,3,3,4),(19.966856329907,20.380981752684,21.3795173426735,22.3780529326629,
23.3765885226523,24.3751241126418,25.3736597026312,26.2500416370866),
 .UNSPECIFIED.);
#341=B_SPLINE_CURVE_WITH_KNOTS('',3,(#16409,#16410,#16411,#16412,#16413,
#16414,#16415,#16416,#16417,#16418,#16419,#16420,#16421,#16422,#16423,#16424,
#16425,#16426,#16427,#16428,#16429,#16430,#16431,#16432,#16433),
 .UNSPECIFIED.,.F.,.F.,(4,3,3,3,3,3,3,3,4),(-35.5088569560286,-35.3346828242492,
-34.3347158943612,-33.3347489644731,-32.3347820345851,-31.3348151046971,
-30.334848174809,-29.334881244921,-29.225671648849),.UNSPECIFIED.);
#342=B_SPLINE_CURVE_WITH_KNOTS('',3,(#16434,#16435,#16436,#16437,#16438,
#16439,#16440,#16441,#16442,#16443,#16444,#16445,#16446,#16447,#16448,#16449,
#16450,#16451,#16452,#16453,#16454,#16455,#16456,#16457,#16458),
 .UNSPECIFIED.,.F.,.F.,(4,3,3,3,3,3,3,3,4),(26.2500416370866,26.3721952926206,
27.37073088261,28.3692664725995,29.3678020625889,30.3663376525783,31.3648732425678,
32.3634088325572,32.5332269442662),.UNSPECIFIED.);
#343=B_SPLINE_CURVE_WITH_KNOTS('',3,(#16463,#16464,#16465,#16466,#16467,
#16468,#16469,#16470,#16471,#16472,#16473,#16474,#16475,#16476,#16477,#16478,
#16479,#16480,#16481,#16482,#16483,#16484),.UNSPECIFIED.,.F.,.F.,(4,3,3,
3,3,3,3,4),(-41.7920422632082,-41.3344844035774,-40.3345174736894,-39.3345505438013,
-38.3345836139133,-37.3346166840253,-36.3346497541372,-35.5088569560286),
 .UNSPECIFIED.);
#344=B_SPLINE_CURVE_WITH_KNOTS('',3,(#16485,#16486,#16487,#16488,#16489,
#16490,#16491,#16492,#16493,#16494,#16495,#16496,#16497,#16498,#16499,#16500,
#16501,#16502,#16503,#16504,#16505,#16506),.UNSPECIFIED.,.F.,.F.,(4,3,3,
3,3,3,3,4),(32.5332269442662,33.3619444225466,34.3604800125361,35.3590156025255,
36.3575511925149,37.3560867825044,38.3546223724938,38.8164122514458),
 .UNSPECIFIED.);
#345=B_SPLINE_CURVE_WITH_KNOTS('',3,(#16511,#16512,#16513,#16514,#16515,
#16516,#16517,#16518,#16519,#16520,#16521,#16522,#16523,#16524,#16525,#16526,
#16527,#16528,#16529,#16530,#16531,#16532),.UNSPECIFIED.,.F.,.F.,(4,3,3,
3,3,3,3,4),(-48.0752275703878,-47.3342859829056,-46.3343190530176,-45.3343521231296,
-44.3343851932415,-43.3344182633535,-42.3344513334655,-41.7920422632082),
 .UNSPECIFIED.);
#346=B_SPLINE_CURVE_WITH_KNOTS('',3,(#16533,#16534,#16535,#16536,#16537,
#16538,#16539,#16540,#16541,#16542,#16543,#16544,#16545,#16546,#16547,#16548,
#16549,#16550,#16551,#16552,#16553,#16554),.UNSPECIFIED.,.F.,.F.,(4,3,3,
3,3,3,3,4),(38.8164122514458,39.3531579624832,40.3516935524726,41.3502291424621,
42.3487647324515,43.3473003224409,44.3458359124304,45.0995975586254),
 .UNSPECIFIED.);
#347=B_SPLINE_CURVE_WITH_KNOTS('',3,(#16561,#16562,#16563,#16564,#16565,
#16566,#16567,#16568,#16569,#16570,#16571,#16572,#16573,#16574,#16575,#16576,
#16577,#16578,#16579,#16580,#16581,#16582,#16583,#16584,#16585,#16586,#16587,
#16588,#16589,#16590,#16591,#16592,#16593,#16594,#16595,#16596,#16597,#16598,
#16599,#16600,#16601,#16602,#16603,#16604,#16605,#16606,#16607,#16608,#16609,
#16610,#16611,#16612,#16613,#16614,#16615,#16616,#16617,#16618,#16619,#16620,
#16621,#16622,#16623,#16624,#16625,#16626,#16627,#16628,#16629,#16630,#16631,
#16632,#16633,#16634,#16635,#16636,#16637,#16638,#16639),.UNSPECIFIED.,
 .F.,.F.,(4,3,3,3,3,3,3,3,3,3,3,3,3,3,3,3,3,3,3,3,3,3,3,3,3,3,4),(-1.51155304937213,
-1.48679926789801,-1.46138770257497,-1.44926072615657,-1.44198354426641,
-1.43723098380472,-1.41129449679306,-1.38512818398721,-1.36854000827839,
-1.36399653483481,-1.33754097405549,-1.31123241658569,-1.28929424823319,
-1.27832516405694,-1.27239106413946,-1.267842943956,-1.26735607988068,-1.24173914861392,
-1.21547146373691,-1.18879082221463,-1.17870805215535,-1.17421497824285,
-1.17020896121405,-1.14333001988911,-1.11622858915333,-1.08943701242486,
-1.07566099703324),.UNSPECIFIED.);
#348=B_SPLINE_CURVE_WITH_KNOTS('',3,(#16642,#16643,#16644,#16645,#16646,
#16647,#16648,#16649,#16650,#16651,#16652,#16653,#16654,#16655,#16656,#16657,
#16658,#16659,#16660,#16661,#16662,#16663,#16664,#16665,#16666,#16667,#16668,
#16669,#16670,#16671,#16672,#16673,#16674,#16675,#16676,#16677,#16678,#16679,
#16680,#16681,#16682,#16683,#16684,#16685,#16686,#16687,#16688,#16689,#16690,
#16691,#16692,#16693,#16694,#16695,#16696,#16697,#16698,#16699,#16700,#16701,
#16702,#16703,#16704,#16705),.UNSPECIFIED.,.F.,.F.,(4,3,3,3,3,3,3,3,3,3,
3,3,3,3,3,3,3,3,3,3,3,4),(-0.41064875043291,-0.381298618400131,-0.351351203500698,
-0.323281054282189,-0.314112148681696,-0.307086254455368,-0.3028330734741,
-0.275277912204971,-0.261508958802399,-0.233266721972606,-0.20410838172603,
-0.199223825603653,-0.195507682996562,-0.168311322654744,-0.141222250485178,
-0.114596755830886,-0.100248696534718,-0.0960146052739596,-0.0702407882655582,
-0.0448488487084018,-0.0202028531448953,0.),.UNSPECIFIED.);
#349=B_SPLINE_CURVE_WITH_KNOTS('',3,(#16706,#16707,#16708,#16709,#16710,
#16711,#16712,#16713,#16714,#16715,#16716,#16717,#16718,#16719,#16720,#16721,
#16722,#16723,#16724,#16725,#16726,#16727,#16728,#16729,#16730,#16731,#16732,
#16733,#16734,#16735,#16736,#16737,#16738,#16739,#16740,#16741,#16742,#16743,
#16744,#16745,#16746,#16747,#16748,#16749,#16750,#16751,#16752,#16753,#16754,
#16755,#16756,#16757,#16758,#16759,#16760,#16761,#16762,#16763,#16764,#16765,
#16766,#16767,#16768,#16769,#16770,#16771,#16772,#16773,#16774,#16775,#16776,
#16777,#16778,#16779,#16780,#16781,#16782,#16783,#16784,#16785,#16786,#16787,
#16788,#16789,#16790,#16791,#16792,#16793,#16794,#16795,#16796,#16797,#16798,
#16799,#16800,#16801,#16802,#16803,#16804,#16805,#16806,#16807,#16808,#16809,
#16810,#16811,#16812,#16813,#16814,#16815,#16816,#16817,#16818,#16819,#16820,
#16821,#16822,#16823,#16824,#16825,#16826,#16827,#16828,#16829,#16830,#16831,
#16832,#16833,#16834,#16835,#16836,#16837,#16838,#16839,#16840,#16841,#16842,
#16843,#16844,#16845,#16846,#16847,#16848,#16849,#16850,#16851,#16852,#16853,
#16854,#16855,#16856,#16857,#16858,#16859,#16860,#16861,#16862,#16863,#16864,
#16865,#16866,#16867,#16868,#16869,#16870,#16871,#16872,#16873,#16874,#16875,
#16876,#16877,#16878,#16879,#16880),.UNSPECIFIED.,.F.,.F.,(4,3,3,3,3,3,
3,3,3,3,3,3,3,3,3,3,3,3,3,3,3,3,3,3,3,3,3,3,3,3,3,3,3,3,3,3,3,3,3,3,3,3,
3,3,3,3,3,3,3,3,3,3,3,3,3,3,3,3,4),(-1.07566099703324,-1.07492144342944,
-1.04755243470394,-1.02055094091712,-1.01298361676725,-0.986089044023807,
-0.977095451514633,-0.97130891557416,-0.943491786406091,-0.915956464286782,
-0.888283595509882,-0.877826699796361,-0.872194960042119,-0.86791902474336,
-0.840054061902339,-0.812175086709734,-0.784725634098613,-0.774568879849767,
-0.769117374745857,-0.765392662069162,-0.748771882229606,-0.721656701079723,
-0.693848162487506,-0.666434123134902,-0.659959284195334,-0.631746794307724,
-0.603158716171934,-0.57463751262923,-0.562124804508911,-0.556268999285474,
-0.552173232275249,-0.52328861334801,-0.494877324909424,-0.474535847666673,
-0.456784896129248,-0.448026129297894,-0.443765804674724,-0.41579810320606,
-0.386811531821062,-0.362275168226913,-0.340805850082031,-0.335237673856059,
-0.30592093381479,-0.276508451915628,-0.247512831305992,-0.23326477924646,
-0.227648927063831,-0.223354867445244,-0.193713728983455,-0.190520623067863,
-0.16154498891856,-0.132023580594298,-0.121964667371235,-0.114890334425799,
-0.110611284048844,-0.0809842299227017,-0.0509674738298579,-0.020991353997103,
0.),.UNSPECIFIED.);
#350=B_SPLINE_CURVE_WITH_KNOTS('',3,(#17094,#17095,#17096,#17097,#17098,
#17099,#17100,#17101,#17102,#17103,#17104,#17105,#17106,#17107,#17108,#17109),
 .UNSPECIFIED.,.F.,.F.,(4,3,3,3,3,4),(-52.3341206323458,-51.3341537024578,
-50.3341867725697,-49.3342198426817,-48.3342529127937,-48.0752275703878),
 .UNSPECIFIED.);
#351=B_SPLINE_CURVE_WITH_KNOTS('',3,(#17110,#17111,#17112,#17113,#17114,
#17115,#17116,#17117,#17118,#17119,#17120,#17121,#17122,#17123,#17124,#17125,
#17126,#17127,#17128,#17129,#17130,#17131,#17132,#17133,#17134,#17135,#17136,
#17137,#17138,#17139,#17140,#17141,#17142,#17143,#17144,#17145,#17146,#17147,
#17148,#17149,#17150,#17151,#17152,#17153,#17154,#17155,#17156,#17157,#17158,
#17159,#17160,#17161,#17162,#17163,#17164,#17165,#17166,#17167,#17168,#17169,
#17170,#17171,#17172,#17173,#17174,#17175,#17176,#17177,#17178,#17179,#17180,
#17181,#17182,#17183,#17184,#17185,#17186,#17187,#17188,#17189,#17190,#17191,
#17192,#17193,#17194,#17195,#17196,#17197,#17198,#17199,#17200),
 .UNSPECIFIED.,.F.,.F.,(4,3,3,3,3,3,3,3,3,3,3,3,3,3,3,3,3,3,3,3,3,3,3,3,
3,3,3,3,3,3,4),(-0.555272788399378,-0.538723215789879,-0.514041682355672,
-0.499599730599056,-0.49342192827285,-0.487658515674462,-0.461864800111998,
-0.439503006879226,-0.428741129403145,-0.42201608450083,-0.395420453364353,
-0.36730795358572,-0.340378564198256,-0.33119785145401,-0.325988107238913,
-0.32191538480378,-0.293998698163474,-0.282970454249821,-0.256042727591499,
-0.228568541876211,-0.221068540885412,-0.216710175387807,-0.188748538124756,
-0.160252201315133,-0.131521042067389,-0.114270249375622,-0.109582556703919,
-0.080105291882733,-0.0505589620440503,-0.0215888429367116,0.),
 .UNSPECIFIED.);
#352=B_SPLINE_CURVE_WITH_KNOTS('',3,(#17201,#17202,#17203,#17204,#17205),
 .UNSPECIFIED.,.F.,.F.,(4,1,4),(13.9508069857623,14.9507739156503,15.707963267949),
 .UNSPECIFIED.);
#353=B_SPLINE_CURVE_WITH_KNOTS('',3,(#17208,#17209,#17210,#17211,#17212,
#17213,#17214,#17215,#17216,#17217,#17218,#17219,#17220,#17221,#17222,#17223,
#17224,#17225,#17226),.UNSPECIFIED.,.F.,.F.,(4,3,3,3,3,3,4),(45.0995975586254,
45.3443715024198,46.3429070924092,47.3414426823987,48.3399782723881,49.3385138623775,
50.2654824574367),.UNSPECIFIED.);
#354=B_SPLINE_CURVE_WITH_KNOTS('',3,(#17469,#17470,#17471,#17472,#17473,
#17474,#17475),.UNSPECIFIED.,.F.,.F.,(4,1,1,1,4),(12.7118898652542,13.7104254552436,
14.7089610452331,15.7074966352225,15.7079632679489),.UNSPECIFIED.);
#355=B_SPLINE_CURVE_WITH_KNOTS('',3,(#17476,#17477,#17478,#17479,#17480,
#17481,#17482,#17483,#17484,#17485,#17486,#17487,#17488,#17489,#17490,#17491,
#17492,#17493,#17494,#17495,#17496,#17497,#17498,#17499,#17500,#17501,#17502,
#17503,#17504,#17505,#17506,#17507,#17508,#17509,#17510,#17511,#17512,#17513,
#17514,#17515,#17516,#17517,#17518,#17519,#17520,#17521,#17522,#17523,#17524,
#17525,#17526,#17527,#17528,#17529,#17530,#17531,#17532,#17533,#17534,#17535,
#17536,#17537,#17538,#17539,#17540,#17541,#17542,#17543,#17544,#17545,#17546,
#17547,#17548,#17549,#17550,#17551,#17552,#17553,#17554,#17555,#17556,#17557,
#17558,#17559,#17560,#17561,#17562,#17563,#17564,#17565,#17566,#17567,#17568,
#17569),.UNSPECIFIED.,.F.,.F.,(4,3,3,3,3,3,3,3,3,3,3,3,3,3,3,3,3,3,3,3,
3,3,3,3,3,3,3,3,3,3,3,4),(-0.552745378375102,-0.531732216109439,-0.502362244303788,
-0.486751274029585,-0.47919381479264,-0.472092376850761,-0.443038187382735,
-0.41923175394946,-0.408411546733614,-0.40204664346163,-0.397482113487408,
-0.369174564086956,-0.340027603044351,-0.312908274838589,-0.297482292749206,
-0.291421604682611,-0.264618441213068,-0.252586719916534,-0.225223404144207,
-0.197070478626181,-0.192533381808034,-0.188242179715238,-0.161600763841001,
-0.135001424894818,-0.108828494157218,-0.0998954833093976,-0.0942242094331416,
-0.0901853384386338,-0.0646415418758646,-0.0395000449170096,-0.0151426917384623,
0.),.UNSPECIFIED.);
#434=SHAPE_REPRESENTATION_RELATIONSHIP('SRR','None',#19952,#453);
#453=ADVANCED_BREP_SHAPE_REPRESENTATION('',(#491),#19861);
#472=STYLED_ITEM('',(#20042),#491);
#491=MANIFOLD_SOLID_BREP('Body1',#6441);
#876=LINE('',#16048,#1341);
#877=LINE('',#16065,#1342);
#878=LINE('',#16090,#1343);
#879=LINE('',#16114,#1344);
#880=LINE('',#16139,#1345);
#881=LINE('',#16164,#1346);
#882=LINE('',#16188,#1347);
#883=LINE('',#16212,#1348);
#884=LINE('',#16237,#1349);
#885=LINE('',#16264,#1350);
#886=LINE('',#16312,#1351);
#887=LINE('',#16360,#1352);
#888=LINE('',#16408,#1353);
#889=LINE('',#16462,#1354);
#890=LINE('',#16510,#1355);
#891=LINE('',#16559,#1356);
#892=LINE('',#17231,#1357);
#893=LINE('',#17233,#1358);
#894=LINE('',#17235,#1359);
#895=LINE('',#17236,#1360);
#896=LINE('',#17239,#1361);
#897=LINE('',#17241,#1362);
#898=LINE('',#17242,#1363);
#899=LINE('',#17245,#1364);
#900=LINE('',#17247,#1365);
#901=LINE('',#17248,#1366);
#902=LINE('',#17251,#1367);
#903=LINE('',#17253,#1368);
#904=LINE('',#17254,#1369);
#905=LINE('',#17257,#1370);
#906=LINE('',#17259,#1371);
#907=LINE('',#17260,#1372);
#908=LINE('',#17262,#1373);
#909=LINE('',#17263,#1374);
#910=LINE('',#17579,#1375);
#911=LINE('',#17585,#1376);
#1341=VECTOR('',#8424,2.37175);
#1342=VECTOR('',#8429,2.37175);
#1343=VECTOR('',#8432,2.37175);
#1344=VECTOR('',#8435,2.37175);
#1345=VECTOR('',#8438,2.37175);
#1346=VECTOR('',#8441,2.37175);
#1347=VECTOR('',#8444,2.37175);
#1348=VECTOR('',#8447,2.37175);
#1349=VECTOR('',#8450,3.);
#1350=VECTOR('',#8455,3.);
#1351=VECTOR('',#8458,3.);
#1352=VECTOR('',#8461,3.);
#1353=VECTOR('',#8464,3.);
#1354=VECTOR('',#8467,3.);
#1355=VECTOR('',#8470,3.);
#1356=VECTOR('',#8475,2.5);
#1357=VECTOR('',#8484,10.);
#1358=VECTOR('',#8485,10.);
#1359=VECTOR('',#8486,10.);
#1360=VECTOR('',#8487,10.);
#1361=VECTOR('',#8490,10.);
#1362=VECTOR('',#8491,10.);
#1363=VECTOR('',#8492,10.);
#1364=VECTOR('',#8495,10.);
#1365=VECTOR('',#8496,10.);
#1366=VECTOR('',#8497,10.);
#1367=VECTOR('',#8500,10.);
#1368=VECTOR('',#8501,10.);
#1369=VECTOR('',#8502,10.);
#1370=VECTOR('',#8505,10.);
#1371=VECTOR('',#8506,10.);
#1372=VECTOR('',#8507,10.);
#1373=VECTOR('',#8510,10.);
#1374=VECTOR('',#8511,10.);
#1375=VECTOR('',#8526,6.);
#1376=VECTOR('',#8535,4.);
#1568=CYLINDRICAL_SURFACE('',#7077,2.37175);
#1569=CYLINDRICAL_SURFACE('',#7079,2.37175);
#1570=CYLINDRICAL_SURFACE('',#7080,2.37175);
#1571=CYLINDRICAL_SURFACE('',#7081,2.37175);
#1572=CYLINDRICAL_SURFACE('',#7082,2.37175);
#1573=CYLINDRICAL_SURFACE('',#7083,2.37175);
#1574=CYLINDRICAL_SURFACE('',#7084,2.37175);
#1575=CYLINDRICAL_SURFACE('',#7085,2.37175);
#1576=CYLINDRICAL_SURFACE('',#7086,2.942);
#1577=CYLINDRICAL_SURFACE('',#7088,2.942);
#1578=CYLINDRICAL_SURFACE('',#7089,2.942);
#1579=CYLINDRICAL_SURFACE('',#7090,2.942);
#1580=CYLINDRICAL_SURFACE('',#7091,2.942);
#1581=CYLINDRICAL_SURFACE('',#7092,2.942);
#1582=CYLINDRICAL_SURFACE('',#7093,2.942);
#1583=CYLINDRICAL_SURFACE('',#7097,2.942);
#1584=CYLINDRICAL_SURFACE('',#7106,2.37175);
#1585=CYLINDRICAL_SURFACE('',#7110,6.);
#1586=CYLINDRICAL_SURFACE('',#7115,4.);
#1682=FACE_BOUND('',#2422,.T.);
#1683=FACE_BOUND('',#2425,.T.);
#1684=FACE_BOUND('',#2427,.T.);
#1970=FACE_OUTER_BOUND('',#2394,.T.);
#1971=FACE_OUTER_BOUND('',#2395,.T.);
#1972=FACE_OUTER_BOUND('',#2396,.T.);
#1973=FACE_OUTER_BOUND('',#2397,.T.);
#1974=FACE_OUTER_BOUND('',#2398,.T.);
#1975=FACE_OUTER_BOUND('',#2399,.T.);
#1976=FACE_OUTER_BOUND('',#2400,.T.);
#1977=FACE_OUTER_BOUND('',#2401,.T.);
#1978=FACE_OUTER_BOUND('',#2402,.T.);
#1979=FACE_OUTER_BOUND('',#2403,.T.);
#1980=FACE_OUTER_BOUND('',#2404,.T.);
#1981=FACE_OUTER_BOUND('',#2405,.T.);
#1982=FACE_OUTER_BOUND('',#2406,.T.);
#1983=FACE_OUTER_BOUND('',#2407,.T.);
#1984=FACE_OUTER_BOUND('',#2408,.T.);
#1985=FACE_OUTER_BOUND('',#2409,.T.);
#1986=FACE_OUTER_BOUND('',#2410,.T.);
#1987=FACE_OUTER_BOUND('',#2411,.T.);
#1988=FACE_OUTER_BOUND('',#2412,.T.);
#1989=FACE_OUTER_BOUND('',#2413,.T.);
#1990=FACE_OUTER_BOUND('',#2414,.T.);
#1991=FACE_OUTER_BOUND('',#2415,.T.);
#1992=FACE_OUTER_BOUND('',#2416,.T.);
#1993=FACE_OUTER_BOUND('',#2417,.T.);
#1994=FACE_OUTER_BOUND('',#2418,.T.);
#1995=FACE_OUTER_BOUND('',#2419,.T.);
#1996=FACE_OUTER_BOUND('',#2420,.T.);
#1997=FACE_OUTER_BOUND('',#2421,.T.);
#1998=FACE_OUTER_BOUND('',#2423,.T.);
#1999=FACE_OUTER_BOUND('',#2424,.T.);
#2000=FACE_OUTER_BOUND('',#2426,.T.);
#2001=FACE_OUTER_BOUND('',#2428,.T.);
#2002=FACE_OUTER_BOUND('',#2429,.T.);
#2394=EDGE_LOOP('',(#5517,#5518,#5519,#5520));
#2395=EDGE_LOOP('',(#5521,#5522,#5523,#5524));
#2396=EDGE_LOOP('',(#5525,#5526,#5527,#5528));
#2397=EDGE_LOOP('',(#5529,#5530,#5531,#5532));
#2398=EDGE_LOOP('',(#5533,#5534,#5535,#5536));
#2399=EDGE_LOOP('',(#5537,#5538,#5539,#5540));
#2400=EDGE_LOOP('',(#5541,#5542,#5543,#5544));
#2401=EDGE_LOOP('',(#5545,#5546,#5547,#5548));
#2402=EDGE_LOOP('',(#5549,#5550,#5551,#5552));
#2403=EDGE_LOOP('',(#5553,#5554,#5555,#5556));
#2404=EDGE_LOOP('',(#5557,#5558,#5559,#5560));
#2405=EDGE_LOOP('',(#5561,#5562,#5563,#5564));
#2406=EDGE_LOOP('',(#5565,#5566,#5567,#5568));
#2407=EDGE_LOOP('',(#5569,#5570,#5571,#5572));
#2408=EDGE_LOOP('',(#5573,#5574,#5575,#5576));
#2409=EDGE_LOOP('',(#5577,#5578,#5579,#5580,#5581,#5582,#5583,#5584));
#2410=EDGE_LOOP('',(#5585,#5586,#5587,#5588,#5589,#5590,#5591,#5592,#5593,
#5594,#5595,#5596,#5597,#5598,#5599,#5600,#5601,#5602,#5603,#5604));
#2411=EDGE_LOOP('',(#5605,#5606,#5607,#5608));
#2412=EDGE_LOOP('',(#5609,#5610,#5611,#5612));
#2413=EDGE_LOOP('',(#5613,#5614,#5615,#5616));
#2414=EDGE_LOOP('',(#5617,#5618,#5619,#5620));
#2415=EDGE_LOOP('',(#5621,#5622,#5623,#5624));
#2416=EDGE_LOOP('',(#5625,#5626,#5627,#5628));
#2417=EDGE_LOOP('',(#5629,#5630,#5631,#5632));
#2418=EDGE_LOOP('',(#5633,#5634,#5635,#5636,#5637,#5638));
#2419=EDGE_LOOP('',(#5639,#5640,#5641,#5642,#5643,#5644,#5645,#5646,#5647,
#5648,#5649,#5650,#5651,#5652,#5653,#5654,#5655,#5656,#5657));
#2420=EDGE_LOOP('',(#5658,#5659,#5660,#5661));
#2421=EDGE_LOOP('',(#5662));
#2422=EDGE_LOOP('',(#5663));
#2423=EDGE_LOOP('',(#5664,#5665,#5666,#5667));
#2424=EDGE_LOOP('',(#5668));
#2425=EDGE_LOOP('',(#5669,#5670,#5671,#5672,#5673,#5674));
#2426=EDGE_LOOP('',(#5675));
#2427=EDGE_LOOP('',(#5676,#5677,#5678,#5679));
#2428=EDGE_LOOP('',(#5680,#5681,#5682,#5683));
#2429=EDGE_LOOP('',(#5684));
#2602=CIRCLE('',#7078,2.37175);
#2603=CIRCLE('',#7087,2.942);
#2604=CIRCLE('',#7095,2.);
#2605=CIRCLE('',#7096,2.37175);
#2606=CIRCLE('',#7098,2.942);
#2607=CIRCLE('',#7108,6.);
#2608=CIRCLE('',#7109,4.);
#2609=CIRCLE('',#7111,6.);
#2610=CIRCLE('',#7114,4.);
#3084=VERTEX_POINT('',#16046);
#3085=VERTEX_POINT('',#16047);
#3086=VERTEX_POINT('',#16049);
#3087=VERTEX_POINT('',#16056);
#3088=VERTEX_POINT('',#16063);
#3089=VERTEX_POINT('',#16064);
#3090=VERTEX_POINT('',#16088);
#3091=VERTEX_POINT('',#16089);
#3092=VERTEX_POINT('',#16112);
#3093=VERTEX_POINT('',#16113);
#3094=VERTEX_POINT('',#16137);
#3095=VERTEX_POINT('',#16138);
#3096=VERTEX_POINT('',#16162);
#3097=VERTEX_POINT('',#16163);
#3098=VERTEX_POINT('',#16186);
#3099=VERTEX_POINT('',#16187);
#3100=VERTEX_POINT('',#16210);
#3101=VERTEX_POINT('',#16211);
#3102=VERTEX_POINT('',#16235);
#3103=VERTEX_POINT('',#16236);
#3104=VERTEX_POINT('',#16238);
#3105=VERTEX_POINT('',#16252);
#3106=VERTEX_POINT('',#16262);
#3107=VERTEX_POINT('',#16263);
#3108=VERTEX_POINT('',#16310);
#3109=VERTEX_POINT('',#16311);
#3110=VERTEX_POINT('',#16358);
#3111=VERTEX_POINT('',#16359);
#3112=VERTEX_POINT('',#16406);
#3113=VERTEX_POINT('',#16407);
#3114=VERTEX_POINT('',#16460);
#3115=VERTEX_POINT('',#16461);
#3116=VERTEX_POINT('',#16508);
#3117=VERTEX_POINT('',#16509);
#3118=VERTEX_POINT('',#16556);
#3119=VERTEX_POINT('',#16558);
#3120=VERTEX_POINT('',#16560);
#3121=VERTEX_POINT('',#16640);
#3122=VERTEX_POINT('',#17093);
#3123=VERTEX_POINT('',#17207);
#3124=VERTEX_POINT('',#17229);
#3125=VERTEX_POINT('',#17230);
#3126=VERTEX_POINT('',#17232);
#3127=VERTEX_POINT('',#17234);
#3128=VERTEX_POINT('',#17238);
#3129=VERTEX_POINT('',#17240);
#3130=VERTEX_POINT('',#17244);
#3131=VERTEX_POINT('',#17246);
#3132=VERTEX_POINT('',#17250);
#3133=VERTEX_POINT('',#17252);
#3134=VERTEX_POINT('',#17256);
#3135=VERTEX_POINT('',#17258);
#3136=VERTEX_POINT('',#17572);
#3137=VERTEX_POINT('',#17574);
#3138=VERTEX_POINT('',#17577);
#3139=VERTEX_POINT('',#17582);
#3917=EDGE_CURVE('',#3084,#3085,#876,.T.);
#3918=EDGE_CURVE('',#3084,#3086,#317,.T.);
#3919=EDGE_CURVE('',#3087,#3086,#2602,.T.);
#3920=EDGE_CURVE('',#3085,#3087,#318,.T.);
#3921=EDGE_CURVE('',#3088,#3089,#877,.T.);
#3922=EDGE_CURVE('',#3088,#3084,#319,.T.);
#3923=EDGE_CURVE('',#3089,#3085,#320,.T.);
#3924=EDGE_CURVE('',#3090,#3091,#878,.T.);
#3925=EDGE_CURVE('',#3090,#3088,#321,.T.);
#3926=EDGE_CURVE('',#3091,#3089,#322,.T.);
#3927=EDGE_CURVE('',#3092,#3093,#879,.T.);
#3928=EDGE_CURVE('',#3092,#3090,#323,.T.);
#3929=EDGE_CURVE('',#3093,#3091,#324,.T.);
#3930=EDGE_CURVE('',#3094,#3095,#880,.T.);
#3931=EDGE_CURVE('',#3094,#3092,#325,.T.);
#3932=EDGE_CURVE('',#3095,#3093,#326,.T.);
#3933=EDGE_CURVE('',#3096,#3097,#881,.T.);
#3934=EDGE_CURVE('',#3096,#3094,#327,.T.);
#3935=EDGE_CURVE('',#3097,#3095,#328,.T.);
#3936=EDGE_CURVE('',#3098,#3099,#882,.T.);
#3937=EDGE_CURVE('',#3098,#3096,#329,.T.);
#3938=EDGE_CURVE('',#3099,#3097,#330,.T.);
#3939=EDGE_CURVE('',#3100,#3101,#883,.T.);
#3940=EDGE_CURVE('',#3100,#3098,#331,.T.);
#3941=EDGE_CURVE('',#3101,#3099,#332,.T.);
#3942=EDGE_CURVE('',#3102,#3103,#884,.T.);
#3943=EDGE_CURVE('',#3102,#3104,#333,.T.);
#3944=EDGE_CURVE('',#3104,#3105,#2603,.T.);
#3945=EDGE_CURVE('',#3105,#3103,#334,.T.);
#3946=EDGE_CURVE('',#3106,#3107,#885,.T.);
#3947=EDGE_CURVE('',#3106,#3102,#335,.T.);
#3948=EDGE_CURVE('',#3103,#3107,#336,.T.);
#3949=EDGE_CURVE('',#3108,#3109,#886,.T.);
#3950=EDGE_CURVE('',#3108,#3106,#337,.T.);
#3951=EDGE_CURVE('',#3107,#3109,#338,.T.);
#3952=EDGE_CURVE('',#3110,#3111,#887,.T.);
#3953=EDGE_CURVE('',#3110,#3108,#339,.T.);
#3954=EDGE_CURVE('',#3109,#3111,#340,.T.);
#3955=EDGE_CURVE('',#3112,#3113,#888,.T.);
#3956=EDGE_CURVE('',#3112,#3110,#341,.T.);
#3957=EDGE_CURVE('',#3111,#3113,#342,.T.);
#3958=EDGE_CURVE('',#3114,#3115,#889,.T.);
#3959=EDGE_CURVE('',#3114,#3112,#343,.T.);
#3960=EDGE_CURVE('',#3113,#3115,#344,.T.);
#3961=EDGE_CURVE('',#3116,#3117,#890,.T.);
#3962=EDGE_CURVE('',#3116,#3114,#345,.T.);
#3963=EDGE_CURVE('',#3115,#3117,#346,.T.);
#3964=EDGE_CURVE('',#3118,#3118,#2604,.T.);
#3965=EDGE_CURVE('',#3118,#3119,#891,.T.);
#3966=EDGE_CURVE('',#3120,#3119,#347,.T.);
#3967=EDGE_CURVE('',#3121,#3120,#2605,.T.);
#3968=EDGE_CURVE('',#3105,#3121,#348,.T.);
#3969=EDGE_CURVE('',#3119,#3104,#349,.T.);
#3970=EDGE_CURVE('',#3122,#3116,#350,.T.);
#3971=EDGE_CURVE('',#3086,#3122,#351,.T.);
#3972=EDGE_CURVE('',#3120,#3100,#352,.T.);
#3973=EDGE_CURVE('',#3117,#3123,#353,.T.);
#3974=EDGE_CURVE('',#3122,#3123,#2606,.F.);
#3975=EDGE_CURVE('',#3124,#3125,#892,.T.);
#3976=EDGE_CURVE('',#3124,#3126,#893,.T.);
#3977=EDGE_CURVE('',#3126,#3127,#894,.T.);
#3978=EDGE_CURVE('',#3125,#3127,#895,.T.);
#3979=EDGE_CURVE('',#3128,#3124,#896,.T.);
#3980=EDGE_CURVE('',#3128,#3129,#897,.T.);
#3981=EDGE_CURVE('',#3129,#3126,#898,.T.);
#3982=EDGE_CURVE('',#3130,#3128,#899,.T.);
#3983=EDGE_CURVE('',#3130,#3131,#900,.T.);
#3984=EDGE_CURVE('',#3131,#3129,#901,.T.);
#3985=EDGE_CURVE('',#3132,#3130,#902,.T.);
#3986=EDGE_CURVE('',#3132,#3133,#903,.T.);
#3987=EDGE_CURVE('',#3133,#3131,#904,.T.);
#3988=EDGE_CURVE('',#3134,#3132,#905,.T.);
#3989=EDGE_CURVE('',#3134,#3135,#906,.T.);
#3990=EDGE_CURVE('',#3135,#3133,#907,.T.);
#3991=EDGE_CURVE('',#3125,#3134,#908,.T.);
#3992=EDGE_CURVE('',#3127,#3135,#909,.T.);
#3993=EDGE_CURVE('',#3121,#3101,#354,.T.);
#3994=EDGE_CURVE('',#3123,#3087,#355,.T.);
#3995=EDGE_CURVE('',#3136,#3136,#2607,.T.);
#3996=EDGE_CURVE('',#3137,#3137,#2608,.T.);
#3997=EDGE_CURVE('',#3138,#3138,#2609,.T.);
#3998=EDGE_CURVE('',#3138,#3136,#910,.T.);
#3999=EDGE_CURVE('',#3139,#3139,#2610,.T.);
#4000=EDGE_CURVE('',#3137,#3139,#911,.T.);
#5517=ORIENTED_EDGE('',*,*,#3917,.F.);
#5518=ORIENTED_EDGE('',*,*,#3918,.T.);
#5519=ORIENTED_EDGE('',*,*,#3919,.F.);
#5520=ORIENTED_EDGE('',*,*,#3920,.F.);
#5521=ORIENTED_EDGE('',*,*,#3921,.F.);
#5522=ORIENTED_EDGE('',*,*,#3922,.T.);
#5523=ORIENTED_EDGE('',*,*,#3917,.T.);
#5524=ORIENTED_EDGE('',*,*,#3923,.F.);
#5525=ORIENTED_EDGE('',*,*,#3924,.F.);
#5526=ORIENTED_EDGE('',*,*,#3925,.T.);
#5527=ORIENTED_EDGE('',*,*,#3921,.T.);
#5528=ORIENTED_EDGE('',*,*,#3926,.F.);
#5529=ORIENTED_EDGE('',*,*,#3927,.F.);
#5530=ORIENTED_EDGE('',*,*,#3928,.T.);
#5531=ORIENTED_EDGE('',*,*,#3924,.T.);
#5532=ORIENTED_EDGE('',*,*,#3929,.F.);
#5533=ORIENTED_EDGE('',*,*,#3930,.F.);
#5534=ORIENTED_EDGE('',*,*,#3931,.T.);
#5535=ORIENTED_EDGE('',*,*,#3927,.T.);
#5536=ORIENTED_EDGE('',*,*,#3932,.F.);
#5537=ORIENTED_EDGE('',*,*,#3933,.F.);
#5538=ORIENTED_EDGE('',*,*,#3934,.T.);
#5539=ORIENTED_EDGE('',*,*,#3930,.T.);
#5540=ORIENTED_EDGE('',*,*,#3935,.F.);
#5541=ORIENTED_EDGE('',*,*,#3936,.F.);
#5542=ORIENTED_EDGE('',*,*,#3937,.T.);
#5543=ORIENTED_EDGE('',*,*,#3933,.T.);
#5544=ORIENTED_EDGE('',*,*,#3938,.F.);
#5545=ORIENTED_EDGE('',*,*,#3939,.F.);
#5546=ORIENTED_EDGE('',*,*,#3940,.T.);
#5547=ORIENTED_EDGE('',*,*,#3936,.T.);
#5548=ORIENTED_EDGE('',*,*,#3941,.F.);
#5549=ORIENTED_EDGE('',*,*,#3942,.F.);
#5550=ORIENTED_EDGE('',*,*,#3943,.T.);
#5551=ORIENTED_EDGE('',*,*,#3944,.T.);
#5552=ORIENTED_EDGE('',*,*,#3945,.T.);
#5553=ORIENTED_EDGE('',*,*,#3946,.F.);
#5554=ORIENTED_EDGE('',*,*,#3947,.T.);
#5555=ORIENTED_EDGE('',*,*,#3942,.T.);
#5556=ORIENTED_EDGE('',*,*,#3948,.T.);
#5557=ORIENTED_EDGE('',*,*,#3949,.F.);
#5558=ORIENTED_EDGE('',*,*,#3950,.T.);
#5559=ORIENTED_EDGE('',*,*,#3946,.T.);
#5560=ORIENTED_EDGE('',*,*,#3951,.T.);
#5561=ORIENTED_EDGE('',*,*,#3952,.F.);
#5562=ORIENTED_EDGE('',*,*,#3953,.T.);
#5563=ORIENTED_EDGE('',*,*,#3949,.T.);
#5564=ORIENTED_EDGE('',*,*,#3954,.T.);
#5565=ORIENTED_EDGE('',*,*,#3955,.F.);
#5566=ORIENTED_EDGE('',*,*,#3956,.T.);
#5567=ORIENTED_EDGE('',*,*,#3952,.T.);
#5568=ORIENTED_EDGE('',*,*,#3957,.T.);
#5569=ORIENTED_EDGE('',*,*,#3958,.F.);
#5570=ORIENTED_EDGE('',*,*,#3959,.T.);
#5571=ORIENTED_EDGE('',*,*,#3955,.T.);
#5572=ORIENTED_EDGE('',*,*,#3960,.T.);
#5573=ORIENTED_EDGE('',*,*,#3961,.F.);
#5574=ORIENTED_EDGE('',*,*,#3962,.T.);
#5575=ORIENTED_EDGE('',*,*,#3958,.T.);
#5576=ORIENTED_EDGE('',*,*,#3963,.T.);
#5577=ORIENTED_EDGE('',*,*,#3964,.F.);
#5578=ORIENTED_EDGE('',*,*,#3965,.T.);
#5579=ORIENTED_EDGE('',*,*,#3966,.F.);
#5580=ORIENTED_EDGE('',*,*,#3967,.F.);
#5581=ORIENTED_EDGE('',*,*,#3968,.F.);
#5582=ORIENTED_EDGE('',*,*,#3944,.F.);
#5583=ORIENTED_EDGE('',*,*,#3969,.F.);
#5584=ORIENTED_EDGE('',*,*,#3965,.F.);
#5585=ORIENTED_EDGE('',*,*,#3966,.T.);
#5586=ORIENTED_EDGE('',*,*,#3969,.T.);
#5587=ORIENTED_EDGE('',*,*,#3943,.F.);
#5588=ORIENTED_EDGE('',*,*,#3947,.F.);
#5589=ORIENTED_EDGE('',*,*,#3950,.F.);
#5590=ORIENTED_EDGE('',*,*,#3953,.F.);
#5591=ORIENTED_EDGE('',*,*,#3956,.F.);
#5592=ORIENTED_EDGE('',*,*,#3959,.F.);
#5593=ORIENTED_EDGE('',*,*,#3962,.F.);
#5594=ORIENTED_EDGE('',*,*,#3970,.F.);
#5595=ORIENTED_EDGE('',*,*,#3971,.F.);
#5596=ORIENTED_EDGE('',*,*,#3918,.F.);
#5597=ORIENTED_EDGE('',*,*,#3922,.F.);
#5598=ORIENTED_EDGE('',*,*,#3925,.F.);
#5599=ORIENTED_EDGE('',*,*,#3928,.F.);
#5600=ORIENTED_EDGE('',*,*,#3931,.F.);
#5601=ORIENTED_EDGE('',*,*,#3934,.F.);
#5602=ORIENTED_EDGE('',*,*,#3937,.F.);
#5603=ORIENTED_EDGE('',*,*,#3940,.F.);
#5604=ORIENTED_EDGE('',*,*,#3972,.F.);
#5605=ORIENTED_EDGE('',*,*,#3961,.T.);
#5606=ORIENTED_EDGE('',*,*,#3973,.T.);
#5607=ORIENTED_EDGE('',*,*,#3974,.F.);
#5608=ORIENTED_EDGE('',*,*,#3970,.T.);
#5609=ORIENTED_EDGE('',*,*,#3975,.F.);
#5610=ORIENTED_EDGE('',*,*,#3976,.T.);
#5611=ORIENTED_EDGE('',*,*,#3977,.T.);
#5612=ORIENTED_EDGE('',*,*,#3978,.F.);
#5613=ORIENTED_EDGE('',*,*,#3979,.F.);
#5614=ORIENTED_EDGE('',*,*,#3980,.T.);
#5615=ORIENTED_EDGE('',*,*,#3981,.T.);
#5616=ORIENTED_EDGE('',*,*,#3976,.F.);
#5617=ORIENTED_EDGE('',*,*,#3982,.F.);
#5618=ORIENTED_EDGE('',*,*,#3983,.T.);
#5619=ORIENTED_EDGE('',*,*,#3984,.T.);
#5620=ORIENTED_EDGE('',*,*,#3980,.F.);
#5621=ORIENTED_EDGE('',*,*,#3985,.F.);
#5622=ORIENTED_EDGE('',*,*,#3986,.T.);
#5623=ORIENTED_EDGE('',*,*,#3987,.T.);
#5624=ORIENTED_EDGE('',*,*,#3983,.F.);
#5625=ORIENTED_EDGE('',*,*,#3988,.F.);
#5626=ORIENTED_EDGE('',*,*,#3989,.T.);
#5627=ORIENTED_EDGE('',*,*,#3990,.T.);
#5628=ORIENTED_EDGE('',*,*,#3986,.F.);
#5629=ORIENTED_EDGE('',*,*,#3991,.F.);
#5630=ORIENTED_EDGE('',*,*,#3978,.T.);
#5631=ORIENTED_EDGE('',*,*,#3992,.T.);
#5632=ORIENTED_EDGE('',*,*,#3989,.F.);
#5633=ORIENTED_EDGE('',*,*,#3992,.F.);
#5634=ORIENTED_EDGE('',*,*,#3977,.F.);
#5635=ORIENTED_EDGE('',*,*,#3981,.F.);
#5636=ORIENTED_EDGE('',*,*,#3984,.F.);
#5637=ORIENTED_EDGE('',*,*,#3987,.F.);
#5638=ORIENTED_EDGE('',*,*,#3990,.F.);
#5639=ORIENTED_EDGE('',*,*,#3968,.T.);
#5640=ORIENTED_EDGE('',*,*,#3993,.T.);
#5641=ORIENTED_EDGE('',*,*,#3941,.T.);
#5642=ORIENTED_EDGE('',*,*,#3938,.T.);
#5643=ORIENTED_EDGE('',*,*,#3935,.T.);
#5644=ORIENTED_EDGE('',*,*,#3932,.T.);
#5645=ORIENTED_EDGE('',*,*,#3929,.T.);
#5646=ORIENTED_EDGE('',*,*,#3926,.T.);
#5647=ORIENTED_EDGE('',*,*,#3923,.T.);
#5648=ORIENTED_EDGE('',*,*,#3920,.T.);
#5649=ORIENTED_EDGE('',*,*,#3994,.F.);
#5650=ORIENTED_EDGE('',*,*,#3973,.F.);
#5651=ORIENTED_EDGE('',*,*,#3963,.F.);
#5652=ORIENTED_EDGE('',*,*,#3960,.F.);
#5653=ORIENTED_EDGE('',*,*,#3957,.F.);
#5654=ORIENTED_EDGE('',*,*,#3954,.F.);
#5655=ORIENTED_EDGE('',*,*,#3951,.F.);
#5656=ORIENTED_EDGE('',*,*,#3948,.F.);
#5657=ORIENTED_EDGE('',*,*,#3945,.F.);
#5658=ORIENTED_EDGE('',*,*,#3939,.T.);
#5659=ORIENTED_EDGE('',*,*,#3993,.F.);
#5660=ORIENTED_EDGE('',*,*,#3967,.T.);
#5661=ORIENTED_EDGE('',*,*,#3972,.T.);
#5662=ORIENTED_EDGE('',*,*,#3995,.F.);
#5663=ORIENTED_EDGE('',*,*,#3996,.T.);
#5664=ORIENTED_EDGE('',*,*,#3997,.F.);
#5665=ORIENTED_EDGE('',*,*,#3998,.T.);
#5666=ORIENTED_EDGE('',*,*,#3995,.T.);
#5667=ORIENTED_EDGE('',*,*,#3998,.F.);
#5668=ORIENTED_EDGE('',*,*,#3997,.T.);
#5669=ORIENTED_EDGE('',*,*,#3975,.T.);
#5670=ORIENTED_EDGE('',*,*,#3991,.T.);
#5671=ORIENTED_EDGE('',*,*,#3988,.T.);
#5672=ORIENTED_EDGE('',*,*,#3985,.T.);
#5673=ORIENTED_EDGE('',*,*,#3982,.T.);
#5674=ORIENTED_EDGE('',*,*,#3979,.T.);
#5675=ORIENTED_EDGE('',*,*,#3999,.F.);
#5676=ORIENTED_EDGE('',*,*,#3974,.T.);
#5677=ORIENTED_EDGE('',*,*,#3994,.T.);
#5678=ORIENTED_EDGE('',*,*,#3919,.T.);
#5679=ORIENTED_EDGE('',*,*,#3971,.T.);
#5680=ORIENTED_EDGE('',*,*,#3996,.F.);
#5681=ORIENTED_EDGE('',*,*,#4000,.T.);
#5682=ORIENTED_EDGE('',*,*,#3999,.T.);
#5683=ORIENTED_EDGE('',*,*,#4000,.F.);
#5684=ORIENTED_EDGE('',*,*,#3964,.T.);
#6045=PLANE('',#7099);
#6046=PLANE('',#7100);
#6047=PLANE('',#7101);
#6048=PLANE('',#7102);
#6049=PLANE('',#7103);
#6050=PLANE('',#7104);
#6051=PLANE('',#7105);
#6052=PLANE('',#7107);
#6053=PLANE('',#7112);
#6054=PLANE('',#7113);
#6055=PLANE('',#7116);
#6349=ADVANCED_FACE('',(#1970),#1568,.T.);
#6350=ADVANCED_FACE('',(#1971),#1569,.T.);
#6351=ADVANCED_FACE('',(#1972),#1570,.T.);
#6352=ADVANCED_FACE('',(#1973),#1571,.T.);
#6353=ADVANCED_FACE('',(#1974),#1572,.T.);
#6354=ADVANCED_FACE('',(#1975),#1573,.T.);
#6355=ADVANCED_FACE('',(#1976),#1574,.T.);
#6356=ADVANCED_FACE('',(#1977),#1575,.T.);
#6357=ADVANCED_FACE('',(#1978),#1576,.T.);
#6358=ADVANCED_FACE('',(#1979),#1577,.T.);
#6359=ADVANCED_FACE('',(#1980),#1578,.T.);
#6360=ADVANCED_FACE('',(#1981),#1579,.T.);
#6361=ADVANCED_FACE('',(#1982),#1580,.T.);
#6362=ADVANCED_FACE('',(#1983),#1581,.T.);
#6363=ADVANCED_FACE('',(#1984),#1582,.T.);
#6364=ADVANCED_FACE('',(#1985),#115,.T.);
#6365=ADVANCED_FACE('',(#1986),#123,.F.);
#6366=ADVANCED_FACE('',(#1987),#1583,.T.);
#6367=ADVANCED_FACE('',(#1988),#6045,.F.);
#6368=ADVANCED_FACE('',(#1989),#6046,.F.);
#6369=ADVANCED_FACE('',(#1990),#6047,.F.);
#6370=ADVANCED_FACE('',(#1991),#6048,.F.);
#6371=ADVANCED_FACE('',(#1992),#6049,.F.);
#6372=ADVANCED_FACE('',(#1993),#6050,.F.);
#6373=ADVANCED_FACE('',(#1994),#6051,.F.);
#6374=ADVANCED_FACE('',(#1995),#124,.F.);
#6375=ADVANCED_FACE('',(#1996),#1584,.T.);
#6376=ADVANCED_FACE('',(#1997,#1682),#6052,.F.);
#6377=ADVANCED_FACE('',(#1998),#1585,.T.);
#6378=ADVANCED_FACE('',(#1999,#1683),#6053,.T.);
#6379=ADVANCED_FACE('',(#2000,#1684),#6054,.F.);
#6380=ADVANCED_FACE('',(#2001),#1586,.T.);
#6381=ADVANCED_FACE('',(#2002),#6055,.F.);
#6441=CLOSED_SHELL('',(#6349,#6350,#6351,#6352,#6353,#6354,#6355,#6356,
#6357,#6358,#6359,#6360,#6361,#6362,#6363,#6364,#6365,#6366,#6367,#6368,
#6369,#6370,#6371,#6372,#6373,#6374,#6375,#6376,#6377,#6378,#6379,#6380,
#6381));
#7076=AXIS2_PLACEMENT_3D('',#16044,#8420,#8421);
#7077=AXIS2_PLACEMENT_3D('',#16045,#8422,#8423);
#7078=AXIS2_PLACEMENT_3D('',#16057,#8425,#8426);
#7079=AXIS2_PLACEMENT_3D('',#16062,#8427,#8428);
#7080=AXIS2_PLACEMENT_3D('',#16087,#8430,#8431);
#7081=AXIS2_PLACEMENT_3D('',#16111,#8433,#8434);
#7082=AXIS2_PLACEMENT_3D('',#16136,#8436,#8437);
#7083=AXIS2_PLACEMENT_3D('',#16161,#8439,#8440);
#7084=AXIS2_PLACEMENT_3D('',#16185,#8442,#8443);
#7085=AXIS2_PLACEMENT_3D('',#16209,#8445,#8446);
#7086=AXIS2_PLACEMENT_3D('',#16234,#8448,#8449);
#7087=AXIS2_PLACEMENT_3D('',#16253,#8451,#8452);
#7088=AXIS2_PLACEMENT_3D('',#16261,#8453,#8454);
#7089=AXIS2_PLACEMENT_3D('',#16309,#8456,#8457);
#7090=AXIS2_PLACEMENT_3D('',#16357,#8459,#8460);
#7091=AXIS2_PLACEMENT_3D('',#16405,#8462,#8463);
#7092=AXIS2_PLACEMENT_3D('',#16459,#8465,#8466);
#7093=AXIS2_PLACEMENT_3D('',#16507,#8468,#8469);
#7094=AXIS2_PLACEMENT_3D('',#16555,#8471,#8472);
#7095=AXIS2_PLACEMENT_3D('',#16557,#8473,#8474);
#7096=AXIS2_PLACEMENT_3D('',#16641,#8476,#8477);
#7097=AXIS2_PLACEMENT_3D('',#17206,#8478,#8479);
#7098=AXIS2_PLACEMENT_3D('',#17227,#8480,#8481);
#7099=AXIS2_PLACEMENT_3D('',#17228,#8482,#8483);
#7100=AXIS2_PLACEMENT_3D('',#17237,#8488,#8489);
#7101=AXIS2_PLACEMENT_3D('',#17243,#8493,#8494);
#7102=AXIS2_PLACEMENT_3D('',#17249,#8498,#8499);
#7103=AXIS2_PLACEMENT_3D('',#17255,#8503,#8504);
#7104=AXIS2_PLACEMENT_3D('',#17261,#8508,#8509);
#7105=AXIS2_PLACEMENT_3D('',#17264,#8512,#8513);
#7106=AXIS2_PLACEMENT_3D('',#17570,#8514,#8515);
#7107=AXIS2_PLACEMENT_3D('',#17571,#8516,#8517);
#7108=AXIS2_PLACEMENT_3D('',#17573,#8518,#8519);
#7109=AXIS2_PLACEMENT_3D('',#17575,#8520,#8521);
#7110=AXIS2_PLACEMENT_3D('',#17576,#8522,#8523);
#7111=AXIS2_PLACEMENT_3D('',#17578,#8524,#8525);
#7112=AXIS2_PLACEMENT_3D('',#17580,#8527,#8528);
#7113=AXIS2_PLACEMENT_3D('',#17581,#8529,#8530);
#7114=AXIS2_PLACEMENT_3D('',#17583,#8531,#8532);
#7115=AXIS2_PLACEMENT_3D('',#17584,#8533,#8534);
#7116=AXIS2_PLACEMENT_3D('',#17586,#8536,#8537);
#8420=DIRECTION('axis',(0.,0.,1.));
#8421=DIRECTION('refdir',(1.,0.,0.));
#8422=DIRECTION('center_axis',(0.,0.,1.));
#8423=DIRECTION('ref_axis',(-0.45781772301594,-0.889046080072625,0.));
#8424=DIRECTION('',(0.,0.,1.));
#8425=DIRECTION('center_axis',(0.,0.,1.));
#8426=DIRECTION('ref_axis',(1.,2.67452657467291E-14,0.));
#8427=DIRECTION('center_axis',(0.,0.,1.));
#8428=DIRECTION('ref_axis',(1.,2.67452657467291E-14,0.));
#8429=DIRECTION('',(0.,0.,1.));
#8430=DIRECTION('center_axis',(0.,0.,1.));
#8431=DIRECTION('ref_axis',(1.,2.67452657467291E-14,0.));
#8432=DIRECTION('',(0.,0.,1.));
#8433=DIRECTION('center_axis',(0.,0.,1.));
#8434=DIRECTION('ref_axis',(1.,2.67452657467291E-14,0.));
#8435=DIRECTION('',(0.,0.,1.));
#8436=DIRECTION('center_axis',(0.,0.,1.));
#8437=DIRECTION('ref_axis',(1.,2.67452657467291E-14,0.));
#8438=DIRECTION('',(0.,0.,1.));
#8439=DIRECTION('center_axis',(0.,0.,1.));
#8440=DIRECTION('ref_axis',(1.,2.67452657467291E-14,0.));
#8441=DIRECTION('',(0.,0.,1.));
#8442=DIRECTION('center_axis',(0.,0.,1.));
#8443=DIRECTION('ref_axis',(1.,2.67452657467291E-14,0.));
#8444=DIRECTION('',(0.,0.,1.));
#8445=DIRECTION('center_axis',(0.,0.,1.));
#8446=DIRECTION('ref_axis',(1.,2.67452657467291E-14,0.));
#8447=DIRECTION('',(0.,0.,1.));
#8448=DIRECTION('center_axis',(0.,0.,1.));
#8449=DIRECTION('ref_axis',(-0.367640013946098,0.929968182329757,0.));
#8450=DIRECTION('',(0.,0.,-1.));
#8451=DIRECTION('center_axis',(0.,0.,1.));
#8452=DIRECTION('ref_axis',(1.,0.,0.));
#8453=DIRECTION('center_axis',(0.,0.,1.));
#8454=DIRECTION('ref_axis',(1.,0.,0.));
#8455=DIRECTION('',(0.,0.,-1.));
#8456=DIRECTION('center_axis',(0.,0.,1.));
#8457=DIRECTION('ref_axis',(1.,0.,0.));
#8458=DIRECTION('',(0.,0.,-1.));
#8459=DIRECTION('center_axis',(0.,0.,1.));
#8460=DIRECTION('ref_axis',(1.,0.,0.));
#8461=DIRECTION('',(0.,0.,-1.));
#8462=DIRECTION('center_axis',(0.,0.,1.));
#8463=DIRECTION('ref_axis',(1.,0.,0.));
#8464=DIRECTION('',(0.,0.,-1.));
#8465=DIRECTION('center_axis',(0.,0.,1.));
#8466=DIRECTION('ref_axis',(1.,0.,0.));
#8467=DIRECTION('',(0.,0.,-1.));
#8468=DIRECTION('center_axis',(0.,0.,1.));
#8469=DIRECTION('ref_axis',(1.,0.,0.));
#8470=DIRECTION('',(0.,0.,-1.));
#8471=DIRECTION('center_axis',(0.,0.,1.));
#8472=DIRECTION('ref_axis',(1.,0.,0.));
#8473=DIRECTION('center_axis',(0.,0.,-1.));
#8474=DIRECTION('ref_axis',(1.,0.,0.));
#8475=DIRECTION('',(-0.707106781186547,-8.65956056235493E-17,0.707106781186548));
#8476=DIRECTION('center_axis',(0.,0.,1.));
#8477=DIRECTION('ref_axis',(1.,2.67452657467291E-14,0.));
#8478=DIRECTION('center_axis',(0.,0.,1.));
#8479=DIRECTION('ref_axis',(1.,0.,0.));
#8480=DIRECTION('center_axis',(0.,0.,-1.));
#8481=DIRECTION('ref_axis',(1.,0.,0.));
#8482=DIRECTION('center_axis',(0.866025403784439,0.5,0.));
#8483=DIRECTION('ref_axis',(0.5,-0.866025403784439,0.));
#8484=DIRECTION('',(0.5,-0.866025403784439,0.));
#8485=DIRECTION('',(0.,0.,-1.));
#8486=DIRECTION('',(0.5,-0.866025403784439,0.));
#8487=DIRECTION('',(0.,0.,-1.));
#8488=DIRECTION('center_axis',(1.20185167898973E-16,1.,0.));
#8489=DIRECTION('ref_axis',(1.,-1.20185167898973E-16,0.));
#8490=DIRECTION('',(1.,-1.20185167898973E-16,0.));
#8491=DIRECTION('',(0.,0.,-1.));
#8492=DIRECTION('',(1.,-1.20185167898973E-16,0.));
#8493=DIRECTION('center_axis',(-0.866025403784439,0.5,0.));
#8494=DIRECTION('ref_axis',(0.5,0.866025403784439,0.));
#8495=DIRECTION('',(0.5,0.866025403784439,0.));
#8496=DIRECTION('',(0.,0.,-1.));
#8497=DIRECTION('',(0.5,0.866025403784439,0.));
#8498=DIRECTION('center_axis',(-0.866025403784439,-0.5,0.));
#8499=DIRECTION('ref_axis',(-0.5,0.866025403784439,0.));
#8500=DIRECTION('',(-0.5,0.866025403784439,0.));
#8501=DIRECTION('',(0.,0.,-1.));
#8502=DIRECTION('',(-0.5,0.866025403784439,0.));
#8503=DIRECTION('center_axis',(-2.40370335797945E-16,-1.,0.));
#8504=DIRECTION('ref_axis',(-1.,2.40370335797945E-16,0.));
#8505=DIRECTION('',(-1.,2.40370335797945E-16,0.));
#8506=DIRECTION('',(0.,0.,-1.));
#8507=DIRECTION('',(-1.,2.40370335797945E-16,0.));
#8508=DIRECTION('center_axis',(0.866025403784439,-0.5,0.));
#8509=DIRECTION('ref_axis',(-0.5,-0.866025403784439,0.));
#8510=DIRECTION('',(-0.5,-0.866025403784439,0.));
#8511=DIRECTION('',(-0.5,-0.866025403784439,0.));
#8512=DIRECTION('center_axis',(0.,0.,-1.));
#8513=DIRECTION('ref_axis',(-1.,0.,0.));
#8514=DIRECTION('center_axis',(0.,0.,1.));
#8515=DIRECTION('ref_axis',(-0.0731438164595877,0.997321403617573,0.));
#8516=DIRECTION('center_axis',(0.,0.,1.));
#8517=DIRECTION('ref_axis',(1.,0.,0.));
#8518=DIRECTION('center_axis',(0.,0.,1.));
#8519=DIRECTION('ref_axis',(1.,0.,0.));
#8520=DIRECTION('center_axis',(0.,0.,1.));
#8521=DIRECTION('ref_axis',(1.,0.,0.));
#8522=DIRECTION('center_axis',(0.,0.,1.));
#8523=DIRECTION('ref_axis',(1.,0.,0.));
#8524=DIRECTION('center_axis',(0.,0.,1.));
#8525=DIRECTION('ref_axis',(1.,0.,0.));
#8526=DIRECTION('',(0.,0.,-1.));
#8527=DIRECTION('center_axis',(0.,0.,1.));
#8528=DIRECTION('ref_axis',(1.,0.,0.));
#8529=DIRECTION('center_axis',(0.,0.,1.));
#8530=DIRECTION('ref_axis',(1.,0.,0.));
#8531=DIRECTION('center_axis',(0.,0.,1.));
#8532=DIRECTION('ref_axis',(1.,0.,0.));
#8533=DIRECTION('center_axis',(0.,0.,1.));
#8534=DIRECTION('ref_axis',(1.,0.,0.));
#8535=DIRECTION('',(0.,0.,-1.));
#8536=DIRECTION('center_axis',(0.,0.,1.));
#8537=DIRECTION('ref_axis',(1.,0.,0.));
#16044=CARTESIAN_POINT('',(0.,0.,0.));
#16045=CARTESIAN_POINT('Origin',(0.,0.,-9.84858989190502));
#16046=CARTESIAN_POINT('',(-2.37107105383284,-0.00233734150670739,-0.348589891905017));
#16047=CARTESIAN_POINT('',(-2.37527615294243,0.000221438259633937,-0.151410108094976));
#16048=CARTESIAN_POINT('',(-2.37175,-6.37235396393925E-14,-9.84858989190502));
#16049=CARTESIAN_POINT('',(1.37999758476545,-1.93379827794526,-6.88317517931686E-16));
#16050=CARTESIAN_POINT('Ctrl Pts',(-2.37107105383284,-0.00233734150670767,
-0.348589891905018));
#16051=CARTESIAN_POINT('Ctrl Pts',(-2.37291097660622,-0.207204195815191,
-0.334848170695028));
#16052=CARTESIAN_POINT('Ctrl Pts',(-2.25467011638231,-1.20079122991256,
-0.268056556211669));
#16053=CARTESIAN_POINT('Ctrl Pts',(-0.903419705864106,-2.62466631852008,
-0.15185992557666));
#16054=CARTESIAN_POINT('Ctrl Pts',(0.780890334042663,-2.35671012203314,
-0.0494050161516468));
#16055=CARTESIAN_POINT('Ctrl Pts',(1.38002164928817,-1.93382042716839,-8.34835672813838E-16));
#16056=CARTESIAN_POINT('',(-1.37702479013102,-1.93106208855765,0.));
#16057=CARTESIAN_POINT('Origin',(0.,0.,0.));
#16058=CARTESIAN_POINT('Ctrl Pts',(-2.37527615294243,0.000221438259633958,
-0.151410108094976));
#16059=CARTESIAN_POINT('Ctrl Pts',(-2.37262065161448,-0.747106869089609,
-0.100940072063317));
#16060=CARTESIAN_POINT('Ctrl Pts',(-1.98938888825771,-1.49439019245279,
-0.0504700360316578));
#16061=CARTESIAN_POINT('Ctrl Pts',(-1.37702479013101,-1.93106208855766,
1.11022302462516E-15));
#16062=CARTESIAN_POINT('Origin',(0.,0.,-9.84858989190502));
#16063=CARTESIAN_POINT('',(-2.36793723488955,0.000550897978577819,-1.34858989190502));
#16064=CARTESIAN_POINT('',(-2.37145569047744,-0.00220250059204397,-1.15141010809498));
#16065=CARTESIAN_POINT('',(-2.37175,-6.37235396393925E-14,-9.84858989190502));
#16066=CARTESIAN_POINT('Ctrl Pts',(-2.36793723488955,0.000550897978577602,
-1.34858989190502));
#16067=CARTESIAN_POINT('Ctrl Pts',(-2.3670439500601,-0.429886149741189,
-1.31981419700191));
#16068=CARTESIAN_POINT('Ctrl Pts',(-2.04853459375008,-1.65509205416319,
-1.23798860882543));
#16069=CARTESIAN_POINT('Ctrl Pts',(-0.0797314402530648,-2.80441033824713,
-1.10311312737558));
#16070=CARTESIAN_POINT('Ctrl Pts',(2.31673231987452,-1.58243891335296,-0.94396344755548));
#16071=CARTESIAN_POINT('Ctrl Pts',(2.58328372722621,1.0944611426978,-0.784813767735368));
#16072=CARTESIAN_POINT('Ctrl Pts',(0.47501218998366,2.76493134210758,-0.625664087915265));
#16073=CARTESIAN_POINT('Ctrl Pts',(-1.85037417679958,1.96916881916604,-0.480256129305143));
#16074=CARTESIAN_POINT('Ctrl Pts',(-2.36580795761266,0.583683975341639,
-0.387898063968396));
#16075=CARTESIAN_POINT('Ctrl Pts',(-2.37107105383284,-0.00233734150670767,
-0.348589891905018));
#16076=CARTESIAN_POINT('Ctrl Pts',(-2.37145569047744,-0.00220250059204391,
-1.15141010809498));
#16077=CARTESIAN_POINT('Ctrl Pts',(-2.37322010983073,-0.195721147004533,
-1.13842444706332));
#16078=CARTESIAN_POINT('Ctrl Pts',(-2.26301140298161,-1.17668930763203,
-1.07246482769833));
#16079=CARTESIAN_POINT('Ctrl Pts',(-0.902039595484687,-2.65503026080224,
-0.953531249999998));
#16080=CARTESIAN_POINT('Ctrl Pts',(1.74372732289156,-2.19643768378856,-0.794609375000001));
#16081=CARTESIAN_POINT('Ctrl Pts',(2.79043291661474,0.277087651255129,-0.635687499999998));
#16082=CARTESIAN_POINT('Ctrl Pts',(1.2788492724039,2.49472256946297,-0.476765624999999));
#16083=CARTESIAN_POINT('Ctrl Pts',(-1.4060176679778,2.42838470324144,-0.317843749999998));
#16084=CARTESIAN_POINT('Ctrl Pts',(-2.35757225025559,0.858781682425109,
-0.209391911031658));
#16085=CARTESIAN_POINT('Ctrl Pts',(-2.37540789782553,0.0372979328012767,
-0.15391403039665));
#16086=CARTESIAN_POINT('Ctrl Pts',(-2.37527615294243,0.000221438259633958,
-0.151410108094976));
#16087=CARTESIAN_POINT('Origin',(0.,0.,-9.84858989190502));
#16088=CARTESIAN_POINT('',(-2.37316232600006,0.00200347480865394,-2.34858989190502));
#16089=CARTESIAN_POINT('',(-2.36793686665521,0.000485999580435575,-2.15141010809498));
#16090=CARTESIAN_POINT('',(-2.37175,-6.37235396393925E-14,-9.84858989190502));
#16091=CARTESIAN_POINT('Ctrl Pts',(-2.37316232600006,0.00200347480865396,
-2.34858989190502));
#16092=CARTESIAN_POINT('Ctrl Pts',(-2.36728640162788,-0.649663311263526,
-2.30478022330879));
#16093=CARTESIAN_POINT('Ctrl Pts',(-1.75058100701069,-2.10021485722012,
-2.2079206614392));
#16094=CARTESIAN_POINT('Ctrl Pts',(0.707590769365126,-2.71486542435539,
-2.05801120629623));
#16095=CARTESIAN_POINT('Ctrl Pts',(2.66676527322589,-0.871519975440165,
-1.89886152647612));
#16096=CARTESIAN_POINT('Ctrl Pts',(2.17427552027739,1.77305104894897,-1.73971184665602));
#16097=CARTESIAN_POINT('Ctrl Pts',(-0.31711023351784,2.787580752663,-1.58056216683591));
#16098=CARTESIAN_POINT('Ctrl Pts',(-2.11921353689182,1.51931384506248,-1.45018818191891));
#16099=CARTESIAN_POINT('Ctrl Pts',(-2.36869077961624,0.363652964407927,
-1.37286409027528));
#16100=CARTESIAN_POINT('Ctrl Pts',(-2.36793723488955,0.000550897978577602,
-1.34858989190502));
#16101=CARTESIAN_POINT('Ctrl Pts',(-2.36793686665521,0.00048599958043568,
-2.15141010809498));
#16102=CARTESIAN_POINT('Ctrl Pts',(-2.36715767925933,-0.425457443633952,
-2.12293486372999));
#16103=CARTESIAN_POINT('Ctrl Pts',(-2.05372327229891,-1.64487463216302,
-2.04148566103166));
#16104=CARTESIAN_POINT('Ctrl Pts',(-0.0995709890729291,-2.80243276783242,
-1.9070625));
#16105=CARTESIAN_POINT('Ctrl Pts',(2.30202865838936,-1.60132637136797,-1.748140625));
#16106=CARTESIAN_POINT('Ctrl Pts',(2.59282079624265,1.06810673697464,-1.58921875));
#16107=CARTESIAN_POINT('Ctrl Pts',(0.506179573027947,2.75812167782342,-1.430296875));
#16108=CARTESIAN_POINT('Ctrl Pts',(-1.83618017076844,1.98774646240115,-1.28436066103166));
#16109=CARTESIAN_POINT('Ctrl Pts',(-2.36602230318261,0.59372258533879,-1.19139840539665));
#16110=CARTESIAN_POINT('Ctrl Pts',(-2.37145569047744,-0.00220250059204391,
-1.15141010809498));
#16111=CARTESIAN_POINT('Origin',(0.,0.,-9.84858989190502));
#16112=CARTESIAN_POINT('',(-2.37454708810461,-0.00146305467787407,-3.34858989190502));
#16113=CARTESIAN_POINT('',(-2.37324810841896,0.00196432295147285,-3.15141010809498));
#16114=CARTESIAN_POINT('',(-2.37175,-6.37235396393925E-14,-9.84858989190502));
#16115=CARTESIAN_POINT('Ctrl Pts',(-2.37454708810461,-0.00146305467787401,
-3.34858989190502));
#16116=CARTESIAN_POINT('Ctrl Pts',(-2.37516922171714,-0.0875139819792011,
-3.34279614288904));
#16117=CARTESIAN_POINT('Ctrl Pts',(-2.33179955053217,-0.960847969556608,
-3.2839525005997));
#16118=CARTESIAN_POINT('Ctrl Pts',(-1.24959461996354,-2.51191054810233,
-3.17205896503699));
#16119=CARTESIAN_POINT('Ctrl Pts',(1.43846132446067,-2.40873623914147,-3.01290928521687));
#16120=CARTESIAN_POINT('Ctrl Pts',(2.80408262807151,-0.0911150253769769,
-2.85375960539677));
#16121=CARTESIAN_POINT('Ctrl Pts',(1.59179933506719,2.3102719050862,-2.69460992557666));
#16122=CARTESIAN_POINT('Ctrl Pts',(-1.08388829677707,2.58773397497002,-2.53546024575656));
#16123=CARTESIAN_POINT('Ctrl Pts',(-2.30086818960063,1.0646887844646,-2.42012023453267));
#16124=CARTESIAN_POINT('Ctrl Pts',(-2.37440166113143,0.139451387812435,
-2.35783011658216));
#16125=CARTESIAN_POINT('Ctrl Pts',(-2.37316232600006,0.00200347480865396,
-2.34858989190502));
#16126=CARTESIAN_POINT('Ctrl Pts',(-2.37324810841896,0.00196432295147262,
-3.15141010809498));
#16127=CARTESIAN_POINT('Ctrl Pts',(-2.36742079101,-0.651949751271476,-3.10744528039665));
#16128=CARTESIAN_POINT('Ctrl Pts',(-1.74738494334323,-2.10348028265193,
-3.01050649436499));
#16129=CARTESIAN_POINT('Ctrl Pts',(0.71129970966804,-2.71249186414424,-2.86059375));
#16130=CARTESIAN_POINT('Ctrl Pts',(2.66552760696098,-0.870932032693957,
-2.701671875));
#16131=CARTESIAN_POINT('Ctrl Pts',(2.17564778740008,1.76921366782114,-2.54275));
#16132=CARTESIAN_POINT('Ctrl Pts',(-0.309153032213342,2.78710993733308,
-2.383828125));
#16133=CARTESIAN_POINT('Ctrl Pts',(-2.11605294401407,1.52493739017563,-2.25338149436499));
#16134=CARTESIAN_POINT('Ctrl Pts',(-2.36860724155681,0.366947001573718,
-2.17590882206332));
#16135=CARTESIAN_POINT('Ctrl Pts',(-2.36793686665521,0.00048599958043568,
-2.15141010809498));
#16136=CARTESIAN_POINT('Origin',(0.,0.,-9.84858989190502));
#16137=CARTESIAN_POINT('',(-2.36855400559966,-0.00132034435408072,-4.34858989190502));
#16138=CARTESIAN_POINT('',(-2.37427834230277,-0.00158579729887448,-4.15141010809498));
#16139=CARTESIAN_POINT('',(-2.37175,-6.37235396393925E-14,-9.84858989190502));
#16140=CARTESIAN_POINT('Ctrl Pts',(-2.36855400559966,-0.00132034435408088,
-4.34858989190502));
#16141=CARTESIAN_POINT('Ctrl Pts',(-2.37012134036242,-0.312665446856959,
-4.32776216919593));
#16142=CARTESIAN_POINT('Ctrl Pts',(-2.16801155330476,-1.41507745062122,
-4.25388455321346));
#16143=CARTESIAN_POINT('Ctrl Pts',(-0.497409040646124,-2.76111672375383,
-4.12695704395763));
#16144=CARTESIAN_POINT('Ctrl Pts',(2.05458518082845,-1.91046094844367,-3.96780736413752));
#16145=CARTESIAN_POINT('Ctrl Pts',(2.717717602526,0.69655748161016,-3.80865768431742));
#16146=CARTESIAN_POINT('Ctrl Pts',(0.882344250202438,2.66320294535576,-3.64950800449731));
#16147=CARTESIAN_POINT('Ctrl Pts',(-1.66785725130337,2.19899767883659,-3.49615207369318));
#16148=CARTESIAN_POINT('Ctrl Pts',(-2.36947271645676,0.700402874070681,
-3.39584603616241));
#16149=CARTESIAN_POINT('Ctrl Pts',(-2.37454708810461,-0.00146305467787401,
-3.34858989190502));
#16150=CARTESIAN_POINT('Ctrl Pts',(-2.37427834230277,-0.00158579729887398,
-4.15141010809498));
#16151=CARTESIAN_POINT('Ctrl Pts',(-2.3750191981319,-0.0978644702926246,
-4.14492965539666));
#16152=CARTESIAN_POINT('Ctrl Pts',(-2.3259543184558,-0.980404337668707,
-4.08547524436499));
#16153=CARTESIAN_POINT('Ctrl Pts',(-1.22000243857572,-2.52490668674665,
-3.973046875));
#16154=CARTESIAN_POINT('Ctrl Pts',(1.46196288604333,-2.39295303517309,-3.814125));
#16155=CARTESIAN_POINT('Ctrl Pts',(2.80340761681022,-0.0668241043267523,
-3.655203125));
#16156=CARTESIAN_POINT('Ctrl Pts',(1.57431810519612,2.32057799752537,-3.49628125));
#16157=CARTESIAN_POINT('Ctrl Pts',(-1.09831409983361,2.58016778763604,-3.337359375));
#16158=CARTESIAN_POINT('Ctrl Pts',(-2.30310126851141,1.05660076494221,-3.22240232769833));
#16159=CARTESIAN_POINT('Ctrl Pts',(-2.37444222349998,0.135962285121762,
-3.16041923872999));
#16160=CARTESIAN_POINT('Ctrl Pts',(-2.37324810841896,0.00196432295147262,
-3.15141010809498));
#16161=CARTESIAN_POINT('Origin',(0.,0.,-9.84858989190502));
#16162=CARTESIAN_POINT('',(-2.36970398032994,0.00191691978235058,-5.34858989190502));
#16163=CARTESIAN_POINT('',(-2.36830943662642,-0.00106730930303889,-5.15141010809498));
#16164=CARTESIAN_POINT('',(-2.37175,-6.37235396393925E-14,-9.84858989190502));
#16165=CARTESIAN_POINT('Ctrl Pts',(-2.36970398032994,0.00191691978235074,
-5.34858989190502));
#16166=CARTESIAN_POINT('Ctrl Pts',(-2.36566369524077,-0.533511972470332,
-5.31272819550281));
#16167=CARTESIAN_POINT('Ctrl Pts',(-1.920436581503,-1.8670796650718,-5.22381660582723));
#16168=CARTESIAN_POINT('Ctrl Pts',(0.294454856588238,-2.79006777499793,
-5.08185512287827));
#16169=CARTESIAN_POINT('Ctrl Pts',(2.50681415110888,-1.25978745570213,-4.92270544305818));
#16170=CARTESIAN_POINT('Ctrl Pts',(2.41455925517875,1.42866531011816,-4.76355576323806));
#16171=CARTESIAN_POINT('Ctrl Pts',(0.102504271982408,2.80368940376361,-4.60440608341796));
#16172=CARTESIAN_POINT('Ctrl Pts',(-1.98887866909948,1.75854255405241,-4.46608412630694));
#16173=CARTESIAN_POINT('Ctrl Pts',(-2.36612921203186,0.480355695668269,
-4.38081206246929));
#16174=CARTESIAN_POINT('Ctrl Pts',(-2.36855400559966,-0.00132034435408088,
-4.34858989190502));
#16175=CARTESIAN_POINT('Ctrl Pts',(-2.36830943662642,-0.00106730930303865,
-5.15141010809498));
#16176=CARTESIAN_POINT('Ctrl Pts',(-2.36964081130378,-0.329574131799768,
-5.12944007206332));
#16177=CARTESIAN_POINT('Ctrl Pts',(-2.15248665188282,-1.44849051785314,
-5.05449607769833));
#16178=CARTESIAN_POINT('Ctrl Pts',(-0.441597707549828,-2.76921495982712,
-4.926578125));
#16179=CARTESIAN_POINT('Ctrl Pts',(2.0888801521554,-1.870865869044,-4.76765625));
#16180=CARTESIAN_POINT('Ctrl Pts',(2.70399705609256,0.742939933921091,-4.608734375));
#16181=CARTESIAN_POINT('Ctrl Pts',(0.839732362462355,2.67552038173531,-4.4498125));
#16182=CARTESIAN_POINT('Ctrl Pts',(-1.68709171325523,2.17606294290117,-4.29737107769833));
#16183=CARTESIAN_POINT('Ctrl Pts',(-2.36896312957456,0.689158080288809,
-4.19790361372999));
#16184=CARTESIAN_POINT('Ctrl Pts',(-2.37427834230277,-0.00158579729887398,
-4.15141010809498));
#16185=CARTESIAN_POINT('Origin',(0.,0.,-9.84858989190502));
#16186=CARTESIAN_POINT('',(-2.37551517139031,0.000588138520267321,-6.34858989190503));
#16187=CARTESIAN_POINT('',(-2.37036013955411,0.00206597193358679,-6.15141010809498));
#16188=CARTESIAN_POINT('',(-2.37175,-6.37235396393925E-14,-9.84858989190502));
#16189=CARTESIAN_POINT('Ctrl Pts',(-2.37551517139031,0.000588138520267192,
-6.34858989190502));
#16190=CARTESIAN_POINT('Ctrl Pts',(-2.37299028602682,-0.75453010380037,
-6.2976942218097));
#16191=CARTESIAN_POINT('Ctrl Pts',(-1.57431214687729,-2.30130303879988,
-6.19374865844099));
#16192=CARTESIAN_POINT('Ctrl Pts',(1.06282132621106,-2.59645975535387,-6.03675320179892));
#16193=CARTESIAN_POINT('Ctrl Pts',(2.75907820786381,-0.508617350322671,
-5.87760352197883));
#16194=CARTESIAN_POINT('Ctrl Pts',(1.91878831253368,2.04680647949509,-5.7184538421587));
#16195=CARTESIAN_POINT('Ctrl Pts',(-0.685511273604884,2.72052538198363,
-5.55930416233861));
#16196=CARTESIAN_POINT('Ctrl Pts',(-2.21477055637751,1.30492154112468,-5.4360161789207));
#16197=CARTESIAN_POINT('Ctrl Pts',(-2.37164045357285,0.258543296497135,
-5.36577808877617));
#16198=CARTESIAN_POINT('Ctrl Pts',(-2.36970398032994,0.00191691978235074,
-5.34858989190502));
#16199=CARTESIAN_POINT('Ctrl Pts',(-2.37036013955411,0.00206597193358676,
-6.15141010809498));
#16200=CARTESIAN_POINT('Ctrl Pts',(-2.36570275369349,-0.5568269279803,-6.11395048872999));
#16201=CARTESIAN_POINT('Ctrl Pts',(-1.88889845039965,-1.9132307197956,-6.02351691103166));
#16202=CARTESIAN_POINT('Ctrl Pts',(0.374189682251391,-2.77913011091259,
-5.88010937499999));
#16203=CARTESIAN_POINT('Ctrl Pts',(2.53898480026785,-1.19042008723587,-5.7211875));
#16204=CARTESIAN_POINT('Ctrl Pts',(2.37571150505774,1.48981793161623,-5.562265625));
#16205=CARTESIAN_POINT('Ctrl Pts',(0.0340680162793398,2.80399746681091,
-5.40334375));
#16206=CARTESIAN_POINT('Ctrl Pts',(-2.01077439008208,1.72085901427313,-5.26639191103166));
#16207=CARTESIAN_POINT('Ctrl Pts',(-2.36643061234994,0.462518639558447,
-5.18241403039665));
#16208=CARTESIAN_POINT('Ctrl Pts',(-2.36830943662642,-0.00106730930303865,
-5.15141010809498));
#16209=CARTESIAN_POINT('Origin',(0.,0.,-9.84858989190502));
#16210=CARTESIAN_POINT('',(-2.37144645257593,-0.00213225654898071,-7.34858989190502));
#16211=CARTESIAN_POINT('',(-2.37545655236239,-0.000153013793341117,-7.15141010809498));
#16212=CARTESIAN_POINT('',(-2.37175,-6.37235396393925E-14,-9.84858989190502));
#16213=CARTESIAN_POINT('Ctrl Pts',(-2.37144645257593,-0.00213225654898062,
-7.34858989190502));
#16214=CARTESIAN_POINT('Ctrl Pts',(-2.37340091284414,-0.194187485402639,
-7.33571014138994));
#16215=CARTESIAN_POINT('Ctrl Pts',(-2.26509829059805,-1.17526209296292,
-7.26978049760149));
#16216=CARTESIAN_POINT('Ctrl Pts',(-0.903098151772226,-2.65539425532298,
-7.15080096053969));
#16217=CARTESIAN_POINT('Ctrl Pts',(1.74597935598366,-2.19600765141715,-6.99165128071957));
#16218=CARTESIAN_POINT('Ctrl Pts',(2.79147243493216,0.283269578050224,-6.83250160089946));
#16219=CARTESIAN_POINT('Ctrl Pts',(1.26983859810019,2.50159785776548,-6.67335192107936));
#16220=CARTESIAN_POINT('Ctrl Pts',(-1.4187825692111,2.42038344679719,-6.51420224125925));
#16221=CARTESIAN_POINT('Ctrl Pts',(-2.36052316049386,0.85148752188555,-6.40594823153447));
#16222=CARTESIAN_POINT('Ctrl Pts',(-2.37562204033538,0.0325494667967356,
-6.35074411508306));
#16223=CARTESIAN_POINT('Ctrl Pts',(-2.37551517139031,0.000588138520267192,
-6.34858989190502));
#16224=CARTESIAN_POINT('Ctrl Pts',(-2.37545655236239,-0.000153013793341093,
-7.15141010809498));
#16225=CARTESIAN_POINT('Ctrl Pts',(-2.37523396052925,-0.785743332277421,
-7.09846090539666));
#16226=CARTESIAN_POINT('Ctrl Pts',(-1.51966847852805,-2.3564332885926,-6.99253774436499));
#16227=CARTESIAN_POINT('Ctrl Pts',(1.15851212495977,-2.55397203032575,-6.833640625));
#16228=CARTESIAN_POINT('Ctrl Pts',(2.77407199314419,-0.40912796830676,-6.67471874999999));
#16229=CARTESIAN_POINT('Ctrl Pts',(1.8463937974617,2.11054799657883,-6.515796875));
#16230=CARTESIAN_POINT('Ctrl Pts',(-0.774509592452447,2.6951571659338,-6.356875));
#16231=CARTESIAN_POINT('Ctrl Pts',(-2.23477737601306,1.2531335513165,-6.23541274436499));
#16232=CARTESIAN_POINT('Ctrl Pts',(-2.37228905031649,0.233537995495179,
-6.16692444706332));
#16233=CARTESIAN_POINT('Ctrl Pts',(-2.37036013955411,0.00206597193358676,
-6.15141010809498));
#16234=CARTESIAN_POINT('Origin',(0.,0.,-8.));
#16235=CARTESIAN_POINT('',(-2.94667044765691,0.000729547181041925,-6.67782388291041));
#16236=CARTESIAN_POINT('',(-2.94659773460531,-0.000189803554299958,-6.8221761170896));
#16237=CARTESIAN_POINT('',(-2.942,-3.60291088309151E-16,-8.));
#16238=CARTESIAN_POINT('',(2.14313711407335,2.01103068470337,-7.058));
#16239=CARTESIAN_POINT('Ctrl Pts',(-2.94667044765691,0.000729547181041925,
-6.67782388291041));
#16240=CARTESIAN_POINT('Ctrl Pts',(-2.94680301155969,0.0403754743611319,
-6.67997810608845));
#16241=CARTESIAN_POINT('Ctrl Pts',(-2.94607214562671,0.0800164233561188,
-6.68213232926648));
#16242=CARTESIAN_POINT('Ctrl Pts',(-2.94446266714682,0.119621710015898,
-6.68428655244452));
#16243=CARTESIAN_POINT('Ctrl Pts',(-2.90482765511341,1.09494137595425,-6.73733644571789));
#16244=CARTESIAN_POINT('Ctrl Pts',(-2.33236709384089,2.04863398522122,-6.79038633899126));
#16245=CARTESIAN_POINT('Ctrl Pts',(-1.49029383690514,2.54227047973339,-6.84343623226463));
#16246=CARTESIAN_POINT('Ctrl Pts',(-0.648220579969394,3.03590697424557,
-6.896486125538));
#16247=CARTESIAN_POINT('Ctrl Pts',(0.463465372629582,3.06948735400294,-6.94953601881137));
#16248=CARTESIAN_POINT('Ctrl Pts',(1.33388947734758,2.62766247069921,-7.00258591208474));
#16249=CARTESIAN_POINT('Ctrl Pts',(1.63696113867246,2.47382412836503,-7.02105727472316));
#16250=CARTESIAN_POINT('Ctrl Pts',(1.91078336440736,2.26234991967576,-7.03952863736158));
#16251=CARTESIAN_POINT('Ctrl Pts',(2.14313711407335,2.01103068470337,-7.058));
#16252=CARTESIAN_POINT('',(-0.260781672665176,2.92495925220595,-7.058));
#16253=CARTESIAN_POINT('Origin',(0.,0.,-7.058));
#16254=CARTESIAN_POINT('Ctrl Pts',(-0.260780188608352,2.92495057073752,
-7.058));
#16255=CARTESIAN_POINT('Ctrl Pts',(-0.734528747633871,2.88336670063893,
-7.03239075299821));
#16256=CARTESIAN_POINT('Ctrl Pts',(-1.19860833266692,2.73328273370447,-7.00678150599641));
#16257=CARTESIAN_POINT('Ctrl Pts',(-1.59511647381414,2.47846404445,-6.98117225899462));
#16258=CARTESIAN_POINT('Ctrl Pts',(-2.41569591362769,1.95111301282311,-6.92817354502628));
#16259=CARTESIAN_POINT('Ctrl Pts',(-2.94687410332821,0.975194558044649,
-6.87517483105794));
#16260=CARTESIAN_POINT('Ctrl Pts',(-2.94659773460531,-0.000189803554299958,
-6.8221761170896));
#16261=CARTESIAN_POINT('Origin',(0.,0.,-8.));
#16262=CARTESIAN_POINT('',(-2.9394620470668,0.00237781300715098,-5.67782388291041));
#16263=CARTESIAN_POINT('',(-2.9402759694606,0.00256270240486823,-5.8221761170896));
#16264=CARTESIAN_POINT('',(-2.942,-3.60291088309151E-16,-8.));
#16265=CARTESIAN_POINT('Ctrl Pts',(-2.9394620470668,0.00237781300715098,
-5.67782388291041));
#16266=CARTESIAN_POINT('Ctrl Pts',(-2.94186411485667,0.32070596744792,-5.69501207978156));
#16267=CARTESIAN_POINT('Ctrl Pts',(-2.89424613177562,0.638334922651543,
-5.71220027665272));
#16268=CARTESIAN_POINT('Ctrl Pts',(-2.79356335203011,0.938143544427409,
-5.72938847352388));
#16269=CARTESIAN_POINT('Ctrl Pts',(-2.48281460043022,1.86347710366387,-5.78243836679725));
#16270=CARTESIAN_POINT('Ctrl Pts',(-1.66657314124927,2.61905502148427,-5.83548826007062));
#16271=CARTESIAN_POINT('Ctrl Pts',(-0.720041998643112,2.85755997694263,
-5.88853815334399));
#16272=CARTESIAN_POINT('Ctrl Pts',(0.226489143963049,3.096064932401,-5.94158804661735));
#16273=CARTESIAN_POINT('Ctrl Pts',(1.30330996999442,2.81749692549733,-5.99463793989072));
#16274=CARTESIAN_POINT('Ctrl Pts',(2.01544111468229,2.14990703628435,-6.04768783316409));
#16275=CARTESIAN_POINT('Ctrl Pts',(2.72757225937017,1.48231714707138,-6.10073772643746));
#16276=CARTESIAN_POINT('Ctrl Pts',(3.07501372271456,0.425705375549109,-6.15378761971083));
#16277=CARTESIAN_POINT('Ctrl Pts',(2.89805192420001,-0.534239058091705,
-6.2068375129842));
#16278=CARTESIAN_POINT('Ctrl Pts',(2.72109012568547,-1.49418349173252,-6.25988740625757));
#16279=CARTESIAN_POINT('Ctrl Pts',(2.01972506531199,-2.35746058749187,-6.31293729953094));
#16280=CARTESIAN_POINT('Ctrl Pts',(1.11636310017402,-2.72724142168666,-6.36598719280431));
#16281=CARTESIAN_POINT('Ctrl Pts',(0.213001135036057,-3.09702225588146,
-6.41903708607767));
#16282=CARTESIAN_POINT('Ctrl Pts',(-0.892357734866394,-2.97330682851169,
-6.47208697935105));
#16283=CARTESIAN_POINT('Ctrl Pts',(-1.69163243842047,-2.41297575352194,
-6.52513687262442));
#16284=CARTESIAN_POINT('Ctrl Pts',(-2.45845059991998,-1.87539831882508,
-6.57603254271975));
#16285=CARTESIAN_POINT('Ctrl Pts',(-2.94353849330279,-0.935945004903834,
-6.62692821281508));
#16286=CARTESIAN_POINT('Ctrl Pts',(-2.94667044765691,0.000729547181041925,
-6.67782388291041));
#16287=CARTESIAN_POINT('Ctrl Pts',(-2.94659773460531,-0.000189803554299958,
-6.8221761170896));
#16288=CARTESIAN_POINT('Ctrl Pts',(-2.94632162406539,-0.97466296344897,
-6.76922691439127));
#16289=CARTESIAN_POINT('Ctrl Pts',(-2.41580926507918,-1.94860411873223,
-6.71627771169294));
#16290=CARTESIAN_POINT('Ctrl Pts',(-1.59710847501959,-2.47650521211642,
-6.66332850899462));
#16291=CARTESIAN_POINT('Ctrl Pts',(-0.778024913229645,-3.00465311803264,
-6.61035455066128));
#16292=CARTESIAN_POINT('Ctrl Pts',(0.329516619306248,-3.08634378537204,
-6.55738059232795));
#16293=CARTESIAN_POINT('Ctrl Pts',(1.217286692148,-2.68376610295237,-6.50440663399462));
#16294=CARTESIAN_POINT('Ctrl Pts',(2.10505676498976,-2.2811884205327,-6.45143267566128));
#16295=CARTESIAN_POINT('Ctrl Pts',(2.77305537813738,-1.39434238835395,-6.39845871732794));
#16296=CARTESIAN_POINT('Ctrl Pts',(2.91526737915637,-0.43000396601087,-6.34548475899461));
#16297=CARTESIAN_POINT('Ctrl Pts',(3.05747938017536,0.534334456332214,-6.29251080066128));
#16298=CARTESIAN_POINT('Ctrl Pts',(2.67390476906572,1.57616526883964,-6.23953684232795));
#16299=CARTESIAN_POINT('Ctrl Pts',(1.94027439593581,2.21794221729091,-6.18656288399462));
#16300=CARTESIAN_POINT('Ctrl Pts',(1.20664402280589,2.85971916574218,-6.13358892566128));
#16301=CARTESIAN_POINT('Ctrl Pts',(0.122957887655704,3.1014422501373,-6.08061496732794));
#16302=CARTESIAN_POINT('Ctrl Pts',(-0.813885412179048,2.8322385802483,-6.02764100899461));
#16303=CARTESIAN_POINT('Ctrl Pts',(-1.7507287120138,2.5630349103593,-5.97466705066128));
#16304=CARTESIAN_POINT('Ctrl Pts',(-2.54072917653311,1.78290448618619,-5.92169309232795));
#16305=CARTESIAN_POINT('Ctrl Pts',(-2.82173256992598,0.849537273856912,
-5.86871913399462));
#16306=CARTESIAN_POINT('Ctrl Pts',(-2.90402926878541,0.576184559247742,
-5.85320479502628));
#16307=CARTESIAN_POINT('Ctrl Pts',(-2.9426686564904,0.289688534941257,-5.83769045605794));
#16308=CARTESIAN_POINT('Ctrl Pts',(-2.9402759694606,0.00256270240486823,
-5.8221761170896));
#16309=CARTESIAN_POINT('Origin',(0.,0.,-8.));
#16310=CARTESIAN_POINT('',(-2.93803557899197,-0.00163780039619282,-4.6778238829104));
#16311=CARTESIAN_POINT('',(-2.9377322072541,-0.00132392704517904,-4.8221761170896));
#16312=CARTESIAN_POINT('',(-2.942,-3.60291088309151E-16,-8.));
#16313=CARTESIAN_POINT('Ctrl Pts',(-2.93803557899197,-0.00163780039619282,
-4.6778238829104));
#16314=CARTESIAN_POINT('Ctrl Pts',(-2.93502778193221,0.595849670773092,
-4.71004605347468));
#16315=CARTESIAN_POINT('Ctrl Pts',(-2.75819953128571,1.19497285403097,-4.74226822403896));
#16316=CARTESIAN_POINT('Ctrl Pts',(-2.41983077500895,1.68182270057143,-4.77449039460323));
#16317=CARTESIAN_POINT('Ctrl Pts',(-1.86274768305156,2.48336188762304,-4.8275402878766));
#16318=CARTESIAN_POINT('Ctrl Pts',(-0.867798935196638,2.98057716514018,
-4.88059018114997));
#16319=CARTESIAN_POINT('Ctrl Pts',(0.107667481214478,2.94491363398168,-4.93364007442334));
#16320=CARTESIAN_POINT('Ctrl Pts',(1.08313389762559,2.90925010282318,-4.98668996769671));
#16321=CARTESIAN_POINT('Ctrl Pts',(2.0391179825929,2.34070776298903,-5.03973986097007));
#16322=CARTESIAN_POINT('Ctrl Pts',(2.53618271428821,1.50062843193614,-5.09278975424345));
#16323=CARTESIAN_POINT('Ctrl Pts',(3.0332474459835,0.660549100883245,-5.14583964751682));
#16324=CARTESIAN_POINT('Ctrl Pts',(3.0713928244068,-0.451067221388398,-5.19888954079019));
#16325=CARTESIAN_POINT('Ctrl Pts',(2.63308446274324,-1.32324407648214,-5.25193943406356));
#16326=CARTESIAN_POINT('Ctrl Pts',(2.19477610107968,-2.19542093157588,-5.30498932733693));
#16327=CARTESIAN_POINT('Ctrl Pts',(1.28001399932924,-2.82815831949173,-5.35803922061029));
#16328=CARTESIAN_POINT('Ctrl Pts',(0.309286933579615,-2.93060579823407,
-5.41108911388366));
#16329=CARTESIAN_POINT('Ctrl Pts',(-0.661440132170006,-3.03305327697642,
-5.46413900715703));
#16330=CARTESIAN_POINT('Ctrl Pts',(-1.68813216191882,-2.60521084654528,
-5.5171889004304));
#16331=CARTESIAN_POINT('Ctrl Pts',(-2.29885015478382,-1.84374503100344,
-5.57023879370377));
#16332=CARTESIAN_POINT('Ctrl Pts',(-2.71169515589689,-1.32899459113155,
-5.60610049010599));
#16333=CARTESIAN_POINT('Ctrl Pts',(-2.93445033894734,-0.661786538635051,
-5.6419621865082));
#16334=CARTESIAN_POINT('Ctrl Pts',(-2.9394620470668,0.00237781300715098,
-5.67782388291041));
#16335=CARTESIAN_POINT('Ctrl Pts',(-2.9402759694606,0.00256270240486823,
-5.8221761170896));
#16336=CARTESIAN_POINT('Ctrl Pts',(-2.93449878839097,-0.690707208650971,
-5.7847164977246));
#16337=CARTESIAN_POINT('Ctrl Pts',(-2.68950923101698,-1.38764883078321,
-5.74725687835961));
#16338=CARTESIAN_POINT('Ctrl Pts',(-2.24226106065643,-1.9121176582849,-5.70979725899461));
#16339=CARTESIAN_POINT('Ctrl Pts',(-1.60977983572761,-2.65380137761201,
-5.65682330066128));
#16340=CARTESIAN_POINT('Ctrl Pts',(-0.572811063603553,-3.05056481578078,
-5.60384934232795));
#16341=CARTESIAN_POINT('Ctrl Pts',(0.393221000839735,-2.92049813954126,
-5.55087538399462));
#16342=CARTESIAN_POINT('Ctrl Pts',(1.35925306528302,-2.79043146330174,-5.49790142566129));
#16343=CARTESIAN_POINT('Ctrl Pts',(2.25434842204554,-2.13353467265391,-5.44492746732795));
#16344=CARTESIAN_POINT('Ctrl Pts',(2.66814113507013,-1.25097642514893,-5.39195350899461));
#16345=CARTESIAN_POINT('Ctrl Pts',(3.08193384809471,-0.368418177643935,
-5.33897955066128));
#16346=CARTESIAN_POINT('Ctrl Pts',(3.01442391738137,0.739801526718225,-5.28600559232795));
#16347=CARTESIAN_POINT('Ctrl Pts',(2.49655981011218,1.56560360282277,-5.23303163399462));
#16348=CARTESIAN_POINT('Ctrl Pts',(1.978695702843,2.39140567892731,-5.18005767566128));
#16349=CARTESIAN_POINT('Ctrl Pts',(1.01047741901797,2.93479012677422,-5.12708371732795));
#16350=CARTESIAN_POINT('Ctrl Pts',(0.0358014650438746,2.94663260578348,
-5.07410975899461));
#16351=CARTESIAN_POINT('Ctrl Pts',(-0.938874488930227,2.95847508479273,
-5.02113580066128));
#16352=CARTESIAN_POINT('Ctrl Pts',(-1.92000811305341,2.4387755949643,-4.96816184232795));
#16353=CARTESIAN_POINT('Ctrl Pts',(-2.45778367776644,1.62579923282352,-4.91518788399462));
#16354=CARTESIAN_POINT('Ctrl Pts',(-2.77252609741322,1.14999080245654,-4.88418396169294));
#16355=CARTESIAN_POINT('Ctrl Pts',(-2.93540164921829,0.573723974947211,
-4.85318003939127));
#16356=CARTESIAN_POINT('Ctrl Pts',(-2.9377322072541,-0.00132392704517904,
-4.8221761170896));
#16357=CARTESIAN_POINT('Origin',(0.,0.,-8.));
#16358=CARTESIAN_POINT('',(-2.9454696039649,-0.00181482317371945,-3.67782388291041));
#16359=CARTESIAN_POINT('',(-2.9451362424601,-0.0019670773281975,-3.8221761170896));
#16360=CARTESIAN_POINT('',(-2.942,-3.60291088309151E-16,-8.));
#16361=CARTESIAN_POINT('Ctrl Pts',(-2.9454696039649,-0.00181482317371945,
-3.67782388291041));
#16362=CARTESIAN_POINT('Ctrl Pts',(-2.93917517943113,0.868803733747646,
-3.7250800271678));
#16363=CARTESIAN_POINT('Ctrl Pts',(-2.5291560477708,1.74457197301595,-3.77233617142519));
#16364=CARTESIAN_POINT('Ctrl Pts',(-1.85306766288973,2.2913421391832,-3.81959231568259));
#16365=CARTESIAN_POINT('Ctrl Pts',(-1.09408875707911,2.90514801387,-3.87264220895595));
#16366=CARTESIAN_POINT('Ctrl Pts',(0.00020064814866938,3.10433811892754,
-3.92569210222932));
#16367=CARTESIAN_POINT('Ctrl Pts',(0.926788687436315,2.79735076364636,-3.97874199550269));
#16368=CARTESIAN_POINT('Ctrl Pts',(1.85337672672397,2.49036340836518,-4.03179188877606));
#16369=CARTESIAN_POINT('Ctrl Pts',(2.61226340007148,1.67719859274527,-4.08484178204943));
#16370=CARTESIAN_POINT('Ctrl Pts',(2.85461137223702,0.731643680721236,-4.1378916753228));
#16371=CARTESIAN_POINT('Ctrl Pts',(3.09695934440256,-0.213911231302795,
-4.19094156859617));
#16372=CARTESIAN_POINT('Ctrl Pts',(2.82276861538611,-1.29185623973094,-4.24399146186954));
#16373=CARTESIAN_POINT('Ctrl Pts',(2.1580763990752,-2.00669250775953,-4.29704135514291));
#16374=CARTESIAN_POINT('Ctrl Pts',(1.49338418276429,-2.72152877578811,-4.35009124841628));
#16375=CARTESIAN_POINT('Ctrl Pts',(0.438190479158908,-3.07325630341714,
-4.40314114168965));
#16376=CARTESIAN_POINT('Ctrl Pts',(-0.522463958417041,-2.90019654199934,
-4.45619103496301));
#16377=CARTESIAN_POINT('Ctrl Pts',(-1.483118395993,-2.72713678058155,-4.50924092823638));
#16378=CARTESIAN_POINT('Ctrl Pts',(-2.34923356753954,-2.02928973011691,
-4.56229082150976));
#16379=CARTESIAN_POINT('Ctrl Pts',(-2.72268243528287,-1.12743465659155,
-4.61534071478313));
#16380=CARTESIAN_POINT('Ctrl Pts',(-2.8693008162719,-0.773360666312599,
-4.63616843749222));
#16381=CARTESIAN_POINT('Ctrl Pts',(-2.93997975475756,-0.387840937979601,
-4.65699616020131));
#16382=CARTESIAN_POINT('Ctrl Pts',(-2.93803557899197,-0.00163780039619282,
-4.6778238829104));
#16383=CARTESIAN_POINT('Ctrl Pts',(-2.9377322072541,-0.00132392704517904,
-4.8221761170896));
#16384=CARTESIAN_POINT('Ctrl Pts',(-2.93938369004142,-0.408815050386763,
-4.80020608105794));
#16385=CARTESIAN_POINT('Ctrl Pts',(-2.86041847102297,-0.815694097620487,
-4.77823604502627));
#16386=CARTESIAN_POINT('Ctrl Pts',(-2.69774861387726,-1.18578124140415,
-4.75626600899461));
#16387=CARTESIAN_POINT('Ctrl Pts',(-2.30552047997214,-2.07813211903793,
-4.70329205066128));
#16388=CARTESIAN_POINT('Ctrl Pts',(-1.42664670685898,-2.75658063985234,
-4.65031809232795));
#16389=CARTESIAN_POINT('Ctrl Pts',(-0.464061240614209,-2.91008106588381,
-4.59734413399462));
#16390=CARTESIAN_POINT('Ctrl Pts',(0.498524225630561,-3.06358149191529,
-4.54437017566128));
#16391=CARTESIAN_POINT('Ctrl Pts',(1.54482138500695,-2.69213382316382,-4.49139621732795));
#16392=CARTESIAN_POINT('Ctrl Pts',(2.19513864684848,-1.96603426957068,-4.43842225899462));
#16393=CARTESIAN_POINT('Ctrl Pts',(2.84545590869002,-1.23993471597753,-4.38544830066128));
#16394=CARTESIAN_POINT('Ctrl Pts',(3.0997932729967,-0.159183277542723,-4.33247434232795));
#16395=CARTESIAN_POINT('Ctrl Pts',(2.84154565012492,0.780732280574893,-4.27950038399461));
#16396=CARTESIAN_POINT('Ctrl Pts',(2.58329802725314,1.72064783869251,-4.22652642566128));
#16397=CARTESIAN_POINT('Ctrl Pts',(1.81246541720289,2.51972751649293,-4.17355246732795));
#16398=CARTESIAN_POINT('Ctrl Pts',(0.882448402231475,2.81162041693353,-4.12057850899462));
#16399=CARTESIAN_POINT('Ctrl Pts',(-0.0475686127399455,3.10351331737414,
-4.06760455066128));
#16400=CARTESIAN_POINT('Ctrl Pts',(-1.13677003263254,2.88821944045492,-4.01463059232795));
#16401=CARTESIAN_POINT('Ctrl Pts',(-1.885794036659,2.26444372326888,-3.96165663399461));
#16402=CARTESIAN_POINT('Ctrl Pts',(-2.54318783632236,1.71697623670729,-3.91516312835961));
#16403=CARTESIAN_POINT('Ctrl Pts',(-2.93854307039457,0.85485530608613,-3.8686696227246));
#16404=CARTESIAN_POINT('Ctrl Pts',(-2.9451362424601,-0.0019670773281975,
-3.8221761170896));
#16405=CARTESIAN_POINT('Origin',(0.,0.,-8.));
#16406=CARTESIAN_POINT('',(-2.94375189758287,0.002485178828774,-2.6778238829104));
#16407=CARTESIAN_POINT('',(-2.94385830503576,0.00243661352308097,-2.8221761170896));
#16408=CARTESIAN_POINT('',(-2.942,-3.60291088309151E-16,-8.));
#16409=CARTESIAN_POINT('Ctrl Pts',(-2.94375189758287,0.002485178828774,
-2.6778238829104));
#16410=CARTESIAN_POINT('Ctrl Pts',(-2.94528921136235,0.172980281625067,
-2.68706410758755));
#16411=CARTESIAN_POINT('Ctrl Pts',(-2.93175845086741,0.343231533938287,
-2.69630433226469));
#16412=CARTESIAN_POINT('Ctrl Pts',(-2.90229484040136,0.510679286112688,
-2.70554455694183));
#16413=CARTESIAN_POINT('Ctrl Pts',(-2.73313862988857,1.47202878702813,-2.7585944502152));
#16414=CARTESIAN_POINT('Ctrl Pts',(-2.03881541363051,2.34097135659234,-2.81164434348857));
#16415=CARTESIAN_POINT('Ctrl Pts',(-1.13848469599121,2.7180803976305,-2.86469423676194));
#16416=CARTESIAN_POINT('Ctrl Pts',(-0.238153978351924,3.09518943866866,
-2.91774413003531));
#16417=CARTESIAN_POINT('Ctrl Pts',(0.868184240668593,2.98046495118077,-2.97079402330868));
#16418=CARTESIAN_POINT('Ctrl Pts',(1.67197964215867,2.42664226336089,-3.02384391658205));
#16419=CARTESIAN_POINT('Ctrl Pts',(2.47577504364874,1.87281957554101,-3.07689380985541));
#16420=CARTESIAN_POINT('Ctrl Pts',(2.97702762760836,0.879898687389133,-3.12994370312878));
#16421=CARTESIAN_POINT('Ctrl Pts',(2.9453266735165,-0.0957045563702386,
-3.18299359640215));
#16422=CARTESIAN_POINT('Ctrl Pts',(2.91362571942463,-1.07130780012962,-3.23604348967552));
#16423=CARTESIAN_POINT('Ctrl Pts',(2.34897122728125,-2.02959339949651,-3.28909338294889));
#16424=CARTESIAN_POINT('Ctrl Pts',(1.51091785855076,-2.53006635742898,-3.34214327622226));
#16425=CARTESIAN_POINT('Ctrl Pts',(0.672864489820277,-3.03053931536144,
-3.39519316949563));
#16426=CARTESIAN_POINT('Ctrl Pts',(-0.438587755497323,-3.0731996318595,
-3.448243062769));
#16427=CARTESIAN_POINT('Ctrl Pts',(-1.31253777493485,-2.63843763607156,
-3.50129295604237));
#16428=CARTESIAN_POINT('Ctrl Pts',(-2.18648779437236,-2.20367564028361,
-3.55434284931574));
#16429=CARTESIAN_POINT('Ctrl Pts',(-2.8229355879298,-1.29149133220967,-3.60739274258911));
#16430=CARTESIAN_POINT('Ctrl Pts',(-2.9293252815118,-0.321188356014672,
-3.66044263586248));
#16431=CARTESIAN_POINT('Ctrl Pts',(-2.94094444122103,-0.215218455480482,
-3.66623638487846));
#16432=CARTESIAN_POINT('Ctrl Pts',(-2.94624131982369,-0.108555343093822,
-3.67203013389443));
#16433=CARTESIAN_POINT('Ctrl Pts',(-2.9454696039649,-0.00181482317371945,
-3.67782388291041));
#16434=CARTESIAN_POINT('Ctrl Pts',(-2.9451362424601,-0.0019670773281975,
-3.8221761170896));
#16435=CARTESIAN_POINT('Ctrl Pts',(-2.94605522542598,-0.121394443596838,
-3.81569566439127));
#16436=CARTESIAN_POINT('Ctrl Pts',(-2.93942137368933,-0.240718870162436,
-3.80921521169294));
#16437=CARTESIAN_POINT('Ctrl Pts',(-2.92489152753265,-0.359073945995959,
-3.80273475899462));
#16438=CARTESIAN_POINT('Ctrl Pts',(-2.80611842621951,-1.3265583406219,-3.74976080066128));
#16439=CARTESIAN_POINT('Ctrl Pts',(-2.15972563543289,-2.22926957242092,
-3.69678684232795));
#16440=CARTESIAN_POINT('Ctrl Pts',(-1.28206228631137,-2.65334521622321,
-3.64381288399462));
#16441=CARTESIAN_POINT('Ctrl Pts',(-0.404398937189858,-3.07742086002551,
-3.59083892566128));
#16442=CARTESIAN_POINT('Ctrl Pts',(0.704534970266555,-3.02286091583108,
-3.53786496732795));
#16443=CARTESIAN_POINT('Ctrl Pts',(1.53633092845112,-2.51467926673377,-3.48489100899462));
#16444=CARTESIAN_POINT('Ctrl Pts',(2.36812688663568,-2.00649761763647,-3.43191705066128));
#16445=CARTESIAN_POINT('Ctrl Pts',(2.9227848955484,-1.04469426363629,-3.37894309232795));
#16446=CARTESIAN_POINT('Ctrl Pts',(2.94601310641574,-0.0702233526915731,
-3.32596913399462));
#16447=CARTESIAN_POINT('Ctrl Pts',(2.96924131728308,0.904247558253159,-3.27299517566128));
#16448=CARTESIAN_POINT('Ctrl Pts',(2.46103973010502,1.89138602614242,-3.22002121732795));
#16449=CARTESIAN_POINT('Ctrl Pts',(1.65440150303174,2.43862260575344,-3.16704725899461));
#16450=CARTESIAN_POINT('Ctrl Pts',(0.847763275958474,2.98585918536446,-3.11407330066128));
#16451=CARTESIAN_POINT('Ctrl Pts',(-0.257311591010001,3.09319387669725,
-3.06109934232795));
#16452=CARTESIAN_POINT('Ctrl Pts',(-1.1541838289695,2.71141738090907,-3.00812538399462));
#16453=CARTESIAN_POINT('Ctrl Pts',(-2.05105606692901,2.32964088512089,-2.95515142566128));
#16454=CARTESIAN_POINT('Ctrl Pts',(-2.73972567587954,1.45875320221174,-2.90217746732795));
#16455=CARTESIAN_POINT('Ctrl Pts',(-2.90446104077339,0.49802672031522,-2.84920350899462));
#16456=CARTESIAN_POINT('Ctrl Pts',(-2.93247711639295,0.334638696232663,
-2.84019437835961));
#16457=CARTESIAN_POINT('Ctrl Pts',(-2.94533952631471,0.168652279046411,
-2.8311852477246));
#16458=CARTESIAN_POINT('Ctrl Pts',(-2.94385830503576,0.00243661352308097,
-2.8221761170896));
#16459=CARTESIAN_POINT('Origin',(0.,0.,-8.));
#16460=CARTESIAN_POINT('',(-2.93727051546118,0.000683352736612908,-1.6778238829104));
#16461=CARTESIAN_POINT('',(-2.93727005869068,0.000602850538960121,-1.8221761170896));
#16462=CARTESIAN_POINT('',(-2.942,-3.60291088309151E-16,-8.));
#16463=CARTESIAN_POINT('Ctrl Pts',(-2.93727051546118,0.000683352736612908,
-1.6778238829104));
#16464=CARTESIAN_POINT('Ctrl Pts',(-2.93820523817054,0.451087602524798,
-1.70209808128066));
#16465=CARTESIAN_POINT('Ctrl Pts',(-2.84105703677905,0.901110116594761,
-1.72637227965093));
#16466=CARTESIAN_POINT('Ctrl Pts',(-2.64374793719726,1.30181149599908,-1.75064647802119));
#16467=CARTESIAN_POINT('Ctrl Pts',(-2.21254001366382,2.17752179084177,-1.80369637129456));
#16468=CARTESIAN_POINT('Ctrl Pts',(-1.30294720868908,2.81766625524686,-1.85674626456792));
#16469=CARTESIAN_POINT('Ctrl Pts',(-0.33308409121168,2.9279955839445,-1.90979615784129));
#16470=CARTESIAN_POINT('Ctrl Pts',(0.636779026265724,3.03832491264213,-1.96284605111466));
#16471=CARTESIAN_POINT('Ctrl Pts',(1.66691245624578,2.6188391056323,-2.01589594438803));
#16472=CARTESIAN_POINT('Ctrl Pts',(2.28379603312924,1.86236011037004,-2.0689458376614));
#16473=CARTESIAN_POINT('Ctrl Pts',(2.90067961001269,1.10588111510779,-2.12199573093477));
#16474=CARTESIAN_POINT('Ctrl Pts',(3.10431333379955,0.0124089315930999,
-2.17504562420814));
#16475=CARTESIAN_POINT('Ctrl Pts',(2.80109232700541,-0.915418640485284,
-2.22809551748151));
#16476=CARTESIAN_POINT('Ctrl Pts',(2.49787132021127,-1.84324621256366,-2.28114541075488));
#16477=CARTESIAN_POINT('Ctrl Pts',(1.68779558283615,-2.60542917320574,-2.33419530402825));
#16478=CARTESIAN_POINT('Ctrl Pts',(0.743232829830214,-2.85161581110816,
-2.38724519730162));
#16479=CARTESIAN_POINT('Ctrl Pts',(-0.201329923175726,-3.09780244901058,
-2.44029509057498));
#16480=CARTESIAN_POINT('Ctrl Pts',(-1.28037969181247,-2.82799276417333,
-2.49334498384836));
#16481=CARTESIAN_POINT('Ctrl Pts',(-1.99790997374708,-2.16620970562137,
-2.54639487712172));
#16482=CARTESIAN_POINT('Ctrl Pts',(-2.59046090871931,-1.61969594868771,
-2.59020454571795));
#16483=CARTESIAN_POINT('Ctrl Pts',(-2.93646319957384,-0.805864640766195,
-2.63401421431418));
#16484=CARTESIAN_POINT('Ctrl Pts',(-2.94375189758287,0.002485178828774,
-2.6778238829104));
#16485=CARTESIAN_POINT('Ctrl Pts',(-2.94385830503576,0.00243661352308097,
-2.8221761170896));
#16486=CARTESIAN_POINT('Ctrl Pts',(-2.93662990077009,-0.808700819327745,
-2.77821128939127));
#16487=CARTESIAN_POINT('Ctrl Pts',(-2.58781232696644,-1.62529773088275,
-2.73424646169294));
#16488=CARTESIAN_POINT('Ctrl Pts',(-1.99154488867446,-2.17202061041561,
-2.69028163399462));
#16489=CARTESIAN_POINT('Ctrl Pts',(-1.27309225084451,-2.83077617836602,
-2.63730767566128));
#16490=CARTESIAN_POINT('Ctrl Pts',(-0.195385854347449,-3.09772203338294,
-2.58433371732795));
#16491=CARTESIAN_POINT('Ctrl Pts',(0.747482555863827,-2.85047263742232,
-2.53135975899461));
#16492=CARTESIAN_POINT('Ctrl Pts',(1.6903509660751,-2.6032232414617,-2.47838580066128));
#16493=CARTESIAN_POINT('Ctrl Pts',(2.49838139000059,-1.84177859452355,-2.42541184232795));
#16494=CARTESIAN_POINT('Ctrl Pts',(2.80111931520967,-0.915235066534927,
-2.37243788399462));
#16495=CARTESIAN_POINT('Ctrl Pts',(3.10385724041874,0.0113084614536957,
-2.31946392566128));
#16496=CARTESIAN_POINT('Ctrl Pts',(2.9013026669114,1.10295087049279,-2.26648996732795));
#16497=CARTESIAN_POINT('Ctrl Pts',(2.28632002818116,1.85921097912,-2.21351600899462));
#16498=CARTESIAN_POINT('Ctrl Pts',(1.67133738945091,2.61547108774722,-2.16054205066128));
#16499=CARTESIAN_POINT('Ctrl Pts',(0.643926685497746,3.03634889596256,-2.10756809232795));
#16500=CARTESIAN_POINT('Ctrl Pts',(-0.324879278745637,2.92888668377361,
-2.05459413399462));
#16501=CARTESIAN_POINT('Ctrl Pts',(-1.29368524298901,2.82142447158467,-2.00162017566128));
#16502=CARTESIAN_POINT('Ctrl Pts',(-2.20388646752261,2.18562223899146,-1.94864621732795));
#16503=CARTESIAN_POINT('Ctrl Pts',(-2.63818645785514,1.31297283747813,-1.89567225899462));
#16504=CARTESIAN_POINT('Ctrl Pts',(-2.83903592378818,0.909401181612935,
-1.87117354502628));
#16505=CARTESIAN_POINT('Ctrl Pts',(-2.93810161469806,0.455173639139868,
-1.84667483105794));
#16506=CARTESIAN_POINT('Ctrl Pts',(-2.93727005869068,0.000602850538960121,
-1.8221761170896));
#16507=CARTESIAN_POINT('Origin',(0.,0.,-8.));
#16508=CARTESIAN_POINT('',(-2.94115781190101,-0.00289931852541142,-0.677823882910403));
#16509=CARTESIAN_POINT('',(-2.94163492837973,-0.00273205723265913,-0.822176117089598));
#16510=CARTESIAN_POINT('',(-2.942,-3.60291088309151E-16,-8.));
#16511=CARTESIAN_POINT('Ctrl Pts',(-2.94115781190101,-0.00289931852541142,
-0.677823882910403));
#16512=CARTESIAN_POINT('Ctrl Pts',(-2.93462928693851,0.724021610816987,
-0.717132054973782));
#16513=CARTESIAN_POINT('Ctrl Pts',(-2.66251292327982,1.45546978445239,-0.756440227037161));
#16514=CARTESIAN_POINT('Ctrl Pts',(-2.17433825692092,1.98917806070832,-0.79574839910054));
#16515=CARTESIAN_POINT('Ctrl Pts',(-1.51550289038833,2.70946510557116,-0.848798292373909));
#16516=CARTESIAN_POINT('Ctrl Pts',(-0.463140743616836,3.06959035999133,
-0.901848185647279));
#16517=CARTESIAN_POINT('Ctrl Pts',(0.498902376961032,2.90430157111178,-0.954898078920648));
#16518=CARTESIAN_POINT('Ctrl Pts',(1.46094549753889,2.73901278223222,-1.00794797219402));
#16519=CARTESIAN_POINT('Ctrl Pts',(2.33266959192314,2.04830995005292,-1.06099786546739));
#16520=CARTESIAN_POINT('Ctrl Pts',(2.71342505533895,1.14953876902873,-1.11404775874076));
#16521=CARTESIAN_POINT('Ctrl Pts',(3.09418051875477,0.250767588004519,-1.16709765201412));
#16522=CARTESIAN_POINT('Ctrl Pts',(2.98396735120216,-0.856071941864584,
-1.22014754528749));
#16523=CARTESIAN_POINT('Ctrl Pts',(2.43341813489043,-1.66212091392741,-1.27319743856086));
#16524=CARTESIAN_POINT('Ctrl Pts',(1.8828689185787,-2.46816988599023,-1.32624733183423));
#16525=CARTESIAN_POINT('Ctrl Pts',(0.891983653507839,-2.97342830024674,
-1.3792972251076));
#16526=CARTESIAN_POINT('Ctrl Pts',(-0.083742367919571,-2.94568489652514,
-1.43234711838097));
#16527=CARTESIAN_POINT('Ctrl Pts',(-1.05946838934697,-2.91794149280355,
-1.48539701165434));
#16528=CARTESIAN_POINT('Ctrl Pts',(-2.02003516713094,-2.35719627110387,
-1.53844690492771));
#16529=CARTESIAN_POINT('Ctrl Pts',(-2.52390703497687,-1.52118559761389,
-1.59149679820108));
#16530=CARTESIAN_POINT('Ctrl Pts',(-2.79722074485897,-1.06771082901965,
-1.62027249310419));
#16531=CARTESIAN_POINT('Ctrl Pts',(-2.93616245433829,-0.533245515985456,
-1.64904818800729));
#16532=CARTESIAN_POINT('Ctrl Pts',(-2.93727051546118,0.000683352736612908,
-1.6778238829104));
#16533=CARTESIAN_POINT('Ctrl Pts',(-2.93727005869068,0.000602850538960121,
-1.8221761170896));
#16534=CARTESIAN_POINT('Ctrl Pts',(-2.93630352793548,-0.527751997120677,
-1.7937008727246));
#16535=CARTESIAN_POINT('Ctrl Pts',(-2.80037799310706,-1.05657056282055,
-1.76522562835961));
#16536=CARTESIAN_POINT('Ctrl Pts',(-2.5324558003079,-1.50684874693044,-1.73675038399462));
#16537=CARTESIAN_POINT('Ctrl Pts',(-2.03402639629669,-2.34452435939227,
-1.68377642566128));
#16538=CARTESIAN_POINT('Ctrl Pts',(-1.07876883214279,-2.91037901388249,
-1.63080246732795));
#16539=CARTESIAN_POINT('Ctrl Pts',(-0.104635629080346,-2.94499075008032,
-1.57782850899462));
#16540=CARTESIAN_POINT('Ctrl Pts',(0.869497573982104,-2.97960248627815,
-1.52485455066128));
#16541=CARTESIAN_POINT('Ctrl Pts',(1.8625064159531,-2.48297130418358,-1.47188059232795));
#16542=CARTESIAN_POINT('Ctrl Pts',(2.4191289262232,-1.68277965785054,-1.41890663399462));
#16543=CARTESIAN_POINT('Ctrl Pts',(2.97575143649328,-0.882588011517496,
-1.36593267566128));
#16544=CARTESIAN_POINT('Ctrl Pts',(3.09598761506247,0.22116409905402,-1.31295871732795));
#16545=CARTESIAN_POINT('Ctrl Pts',(2.7247154876507,1.12243223163693,-1.25998475899462));
#16546=CARTESIAN_POINT('Ctrl Pts',(2.35344336023893,2.02370036421984,-1.20701080066128));
#16547=CARTESIAN_POINT('Ctrl Pts',(1.4906629268462,2.72248451881415,-1.15403684232795));
#16548=CARTESIAN_POINT('Ctrl Pts',(0.531925431096018,2.89843813313422,-1.10106288399462));
#16549=CARTESIAN_POINT('Ctrl Pts',(-0.426812064654162,3.0743917474543,-1.04808892566128));
#16550=CARTESIAN_POINT('Ctrl Pts',(-1.48150662276179,2.72751482150015,-0.995114967327949));
#16551=CARTESIAN_POINT('Ctrl Pts',(-2.14860846972942,2.01679609366237,-0.942141008994616));
#16552=CARTESIAN_POINT('Ctrl Pts',(-2.65218169374977,1.48029792209265,-0.902152711692943));
#16553=CARTESIAN_POINT('Ctrl Pts',(-2.93489516853091,0.736473846765843,
-0.86216441439127));
#16554=CARTESIAN_POINT('Ctrl Pts',(-2.94163492837973,-0.00273205723265913,
-0.822176117089598));
#16555=CARTESIAN_POINT('Origin',(0.,0.,-7.5));
#16556=CARTESIAN_POINT('',(-2.,-2.44929359829471E-16,-8.));
#16557=CARTESIAN_POINT('Origin',(0.,0.,-8.));
#16558=CARTESIAN_POINT('',(-2.54872116535053,-0.00229165091991151,-7.45095259589208));
#16559=CARTESIAN_POINT('',(-2.5,-3.06161699786838E-16,-7.5));
#16560=CARTESIAN_POINT('',(0.43944522199408,2.3306835819919,-7.62825));
#16561=CARTESIAN_POINT('Ctrl Pts',(0.439445221994064,2.3306835819919,-7.62825));
#16562=CARTESIAN_POINT('Ctrl Pts',(0.35950730762982,2.34930583235909,-7.62476133607378));
#16563=CARTESIAN_POINT('Ctrl Pts',(0.278764199343595,2.36340008398443,-7.62128689705201));
#16564=CARTESIAN_POINT('Ctrl Pts',(0.19754033703868,2.37315335070148,-7.61782195797437));
#16565=CARTESIAN_POINT('Ctrl Pts',(0.114158107745347,2.38316579161086,-7.61426494484472));
#16566=CARTESIAN_POINT('Ctrl Pts',(0.0302684811334496,2.38860350484577,
-7.61071794325263));
#16567=CARTESIAN_POINT('Ctrl Pts',(-0.0537928869498894,2.38961650778545,
-7.60717584146979));
#16568=CARTESIAN_POINT('Ctrl Pts',(-0.0939088819893571,2.3900999358075,
-7.60548547000916));
#16569=CARTESIAN_POINT('Ctrl Pts',(-0.134064139304447,2.38957491574745,
-7.60379621443857));
#16570=CARTESIAN_POINT('Ctrl Pts',(-0.174222567562762,2.38805369630578,
-7.60210751919786));
#16571=CARTESIAN_POINT('Ctrl Pts',(-0.198320922896885,2.38714083969668,
-7.60109416335384));
#16572=CARTESIAN_POINT('Ctrl Pts',(-0.222420421447383,2.3858692035713,-7.60008100928382));
#16573=CARTESIAN_POINT('Ctrl Pts',(-0.246513240972343,2.38424099601516,
-7.59906793693749));
#16574=CARTESIAN_POINT('Ctrl Pts',(-0.262247708409472,2.38317765103196,
-7.59840632264082));
#16575=CARTESIAN_POINT('Ctrl Pts',(-0.277979991167122,2.38196207006022,
-7.59774471512093));
#16576=CARTESIAN_POINT('Ctrl Pts',(-0.2936918680985,2.38059645837412,-7.59708375573829));
#16577=CARTESIAN_POINT('Ctrl Pts',(-0.379437414156161,2.37314380836678,
-7.59347665498045));
#16578=CARTESIAN_POINT('Ctrl Pts',(-0.464688261375226,2.36122031408759,
-7.58988407990206));
#16579=CARTESIAN_POINT('Ctrl Pts',(-0.549092376979852,2.34499084734367,
-7.58630079485361));
#16580=CARTESIAN_POINT('Ctrl Pts',(-0.634244405857918,2.32861756967879,
-7.58268575795952));
#16581=CARTESIAN_POINT('Ctrl Pts',(-0.718535581092846,2.30786151927559,
-7.57908017646459));
#16582=CARTESIAN_POINT('Ctrl Pts',(-0.801603640347307,2.28283889337961,
-7.57547867430154));
#16583=CARTESIAN_POINT('Ctrl Pts',(-0.854264768910885,2.26697575981018,
-7.57319549626497));
#16584=CARTESIAN_POINT('Ctrl Pts',(-0.906434273693594,2.24939685671676,
-7.57091395768995));
#16585=CARTESIAN_POINT('Ctrl Pts',(-0.958017010478469,2.23012130716734,
-7.56863268885273));
#16586=CARTESIAN_POINT('Ctrl Pts',(-0.972145435378402,2.22484176654604,
-7.5680078531528));
#16587=CARTESIAN_POINT('Ctrl Pts',(-0.98622277804679,2.21943748744756,-7.56738334854454));
#16588=CARTESIAN_POINT('Ctrl Pts',(-1.00024110670404,2.21391165688255,-7.56675941869597));
#16589=CARTESIAN_POINT('Ctrl Pts',(-1.08186648658626,2.18173606519387,-7.56312642419607));
#16590=CARTESIAN_POINT('Ctrl Pts',(-1.16155672144445,2.14541925679892,-7.55951003039887));
#16591=CARTESIAN_POINT('Ctrl Pts',(-1.2389527254794,2.10510908910794,-7.55590492027959));
#16592=CARTESIAN_POINT('Ctrl Pts',(-1.31591866988219,2.06502290941356,-7.55231984236159));
#16593=CARTESIAN_POINT('Ctrl Pts',(-1.390616753222,2.0209873367507,-7.54874592307184));
#16594=CARTESIAN_POINT('Ctrl Pts',(-1.4626804776292,1.97309843650394,-7.5451779335279));
#16595=CARTESIAN_POINT('Ctrl Pts',(-1.5227729444993,1.93316486139114,-7.54220265997348));
#16596=CARTESIAN_POINT('Ctrl Pts',(-1.58103363744146,1.89055092502882,-7.53923150969818));
#16597=CARTESIAN_POINT('Ctrl Pts',(-1.63723570611631,1.84528793751806,-7.53626145077414));
#16598=CARTESIAN_POINT('Ctrl Pts',(-1.66533674045373,1.82265644376269,-7.53477642131212));
#16599=CARTESIAN_POINT('Ctrl Pts',(-1.69292287318535,1.79936235037773,-7.53329166468791));
#16600=CARTESIAN_POINT('Ctrl Pts',(-1.71996402237359,1.77540760445319,-7.53180680191054));
#16601=CARTESIAN_POINT('Ctrl Pts',(-1.734592853604,1.76244846825458,-7.53100351478619));
#16602=CARTESIAN_POINT('Ctrl Pts',(-1.74906216596862,1.74929596081963,-7.53020019659465));
#16603=CARTESIAN_POINT('Ctrl Pts',(-1.76336702959904,1.73595023612016,-7.52939678733164));
#16604=CARTESIAN_POINT('Ctrl Pts',(-1.77433082190178,1.72572156442395,-7.52878102387374));
#16605=CARTESIAN_POINT('Ctrl Pts',(-1.78519228949581,1.71538465010188,-7.52816552606711));
#16606=CARTESIAN_POINT('Ctrl Pts',(-1.79594364956077,1.70494575402236,-7.52755060631426));
#16607=CARTESIAN_POINT('Ctrl Pts',(-1.79709455383888,1.7038282981764,-7.52748478080288));
#16608=CARTESIAN_POINT('Ctrl Pts',(-1.79824421789083,1.70270965364318,-7.52741896070807));
#16609=CARTESIAN_POINT('Ctrl Pts',(-1.79939263955324,1.70158982119388,-7.52735314599821));
#16610=CARTESIAN_POINT('Ctrl Pts',(-1.85981820858233,1.64266850754977,-7.52389022691203));
#16611=CARTESIAN_POINT('Ctrl Pts',(-1.91680672394307,1.58046245918003,-7.52044221587196));
#16612=CARTESIAN_POINT('Ctrl Pts',(-1.97033907896298,1.51537581293649,-7.51700450873067));
#16613=CARTESIAN_POINT('Ctrl Pts',(-2.02523133040966,1.44863575358186,-7.51347947261505));
#16614=CARTESIAN_POINT('Ctrl Pts',(-2.07649002117627,1.37886624042406,-7.50996527055285));
#16615=CARTESIAN_POINT('Ctrl Pts',(-2.12405982073786,1.30645857743699,-7.50645693852668));
#16616=CARTESIAN_POINT('Ctrl Pts',(-2.17237746941273,1.23291258704349,-7.502893451696));
#16617=CARTESIAN_POINT('Ctrl Pts',(-2.21688976450887,1.15664403526371,-7.49933602091887));
#16618=CARTESIAN_POINT('Ctrl Pts',(-2.25749682318216,1.07802895465018,-7.49577944435867));
#16619=CARTESIAN_POINT('Ctrl Pts',(-2.27284246751551,1.04831985712508,-7.49443539333109));
#16620=CARTESIAN_POINT('Ctrl Pts',(-2.28762993718892,1.0182753662529,-7.49309146429663));
#16621=CARTESIAN_POINT('Ctrl Pts',(-2.30185211585003,0.987914916938409,
-7.49174737651324));
#16622=CARTESIAN_POINT('Ctrl Pts',(-2.30818978888486,0.974385723870973,
-7.49114842545909));
#16623=CARTESIAN_POINT('Ctrl Pts',(-2.31441519544955,0.960793784042873,
-7.49054944288118));
#16624=CARTESIAN_POINT('Ctrl Pts',(-2.32052764172134,0.947140796183267,
-7.48995040393679));
#16625=CARTESIAN_POINT('Ctrl Pts',(-2.32597748838073,0.934967815519079,
-7.4894163018368));
#16626=CARTESIAN_POINT('Ctrl Pts',(-2.33133358181014,0.922755126093933,
-7.48888254203352));
#16627=CARTESIAN_POINT('Ctrl Pts',(-2.33659539015647,0.910505115445706,
-7.48834914975349));
#16628=CARTESIAN_POINT('Ctrl Pts',(-2.37190024202985,0.828311925782129,
-7.484770278347));
#16629=CARTESIAN_POINT('Ctrl Pts',(-2.40297018516154,0.744427201867178,
-7.48120732731796));
#16630=CARTESIAN_POINT('Ctrl Pts',(-2.4297508852343,0.659261131816419,-7.47765521995893));
#16631=CARTESIAN_POINT('Ctrl Pts',(-2.4567532615297,0.573390102871637,-7.47407371016681));
#16632=CARTESIAN_POINT('Ctrl Pts',(-2.47939547698255,0.486215506233761,
-7.4705032243038));
#16633=CARTESIAN_POINT('Ctrl Pts',(-2.49757659361956,0.39812982730928,-7.46693855854928));
#16634=CARTESIAN_POINT('Ctrl Pts',(-2.51554984330289,0.311051242839216,
-7.46341464805892));
#16635=CARTESIAN_POINT('Ctrl Pts',(-2.52916366178314,0.223081332246028,
-7.4598964253538));
#16636=CARTESIAN_POINT('Ctrl Pts',(-2.53827206334785,0.134586184014785,
-7.4563788630682));
#16637=CARTESIAN_POINT('Ctrl Pts',(-2.54295553089513,0.0890826835499858,
-7.45457016055402));
#16638=CARTESIAN_POINT('Ctrl Pts',(-2.54644698417321,0.043440188370138,
-7.45276163265044));
#16639=CARTESIAN_POINT('Ctrl Pts',(-2.54872116535053,-0.00229165091991107,
-7.45095259589208));
#16640=CARTESIAN_POINT('',(2.34668236863854,0.343918483395443,-7.62825));
#16641=CARTESIAN_POINT('Origin',(0.,0.,-7.62825));
#16642=CARTESIAN_POINT('Ctrl Pts',(-0.260780188608367,2.92495057073752,
-7.058));
#16643=CARTESIAN_POINT('Ctrl Pts',(-0.16290664670437,2.92113933331557,-7.07037763567872));
#16644=CARTESIAN_POINT('Ctrl Pts',(-0.0655009153188213,2.91268382038242,
-7.08279941895993));
#16645=CARTESIAN_POINT('Ctrl Pts',(0.0310593059060548,2.89959286742514,
-7.09528489244389));
#16646=CARTESIAN_POINT('Ctrl Pts',(0.129584552898908,2.88623551014979,-7.10802444858021));
#16647=CARTESIAN_POINT('Ctrl Pts',(0.227230615089889,2.86805205167427,-7.12083031352007));
#16648=CARTESIAN_POINT('Ctrl Pts',(0.323572833643809,2.84500022309371,-7.13372324739925));
#16649=CARTESIAN_POINT('Ctrl Pts',(0.413875801694046,2.82339340760767,-7.14580798256147));
#16650=CARTESIAN_POINT('Ctrl Pts',(0.503033721796121,2.79750880812771,-7.15796921289429));
#16651=CARTESIAN_POINT('Ctrl Pts',(0.590666117804777,2.76727297965209,-7.17022403407592));
#16652=CARTESIAN_POINT('Ctrl Pts',(0.619290588600912,2.75739667101947,-7.17422698032642));
#16653=CARTESIAN_POINT('Ctrl Pts',(0.647752008816874,2.74705582179321,-7.17823991228686));
#16654=CARTESIAN_POINT('Ctrl Pts',(0.67603622728258,2.73624706112264,-7.18226342576295));
#16655=CARTESIAN_POINT('Ctrl Pts',(0.697709689293547,2.72796458854652,-7.18534653964076));
#16656=CARTESIAN_POINT('Ctrl Pts',(0.719279093667969,2.7194073616259,-7.18843586672941));
#16657=CARTESIAN_POINT('Ctrl Pts',(0.740737874893652,2.71057371154558,-7.19153167510431));
#16658=CARTESIAN_POINT('Ctrl Pts',(0.753728118875441,2.70522619117216,-7.19340574734018));
#16659=CARTESIAN_POINT('Ctrl Pts',(0.766677009772667,2.69977763294854,-7.19528208283154));
#16660=CARTESIAN_POINT('Ctrl Pts',(0.779571505380582,2.69423287115845,-7.19715904078809));
#16661=CARTESIAN_POINT('Ctrl Pts',(0.863111309476644,2.65830992172418,-7.20931932256682));
#16662=CARTESIAN_POINT('Ctrl Pts',(0.944501853536966,2.61829878211877,-7.22152465472504));
#16663=CARTESIAN_POINT('Ctrl Pts',(1.02341032522997,2.57417267578142,-7.23379399917205));
#16664=CARTESIAN_POINT('Ctrl Pts',(1.06283985566158,2.55212343803384,-7.2399248299925));
#16665=CARTESIAN_POINT('Ctrl Pts',(1.10164917691728,2.52904610718385,-7.24607164384984));
#16666=CARTESIAN_POINT('Ctrl Pts',(1.13979350230052,2.50493366123382,-7.25223680653294));
#16667=CARTESIAN_POINT('Ctrl Pts',(1.21803336844641,2.45547533356318,-7.26488250148881));
#16668=CARTESIAN_POINT('Ctrl Pts',(1.29347831788253,2.40166348524667,-7.27760539418667));
#16669=CARTESIAN_POINT('Ctrl Pts',(1.36591536301843,2.3438254012589,-7.29042590061749));
#16670=CARTESIAN_POINT('Ctrl Pts',(1.44070207418648,2.284111202901,-7.30366227034614));
#16671=CARTESIAN_POINT('Ctrl Pts',(1.51228330084963,2.2201043116401,-7.31700268917746));
#16672=CARTESIAN_POINT('Ctrl Pts',(1.58037036975762,2.15214475623283,-7.33046962496539));
#16673=CARTESIAN_POINT('Ctrl Pts',(1.59177620103872,2.14076028579893,-7.33272558340116));
#16674=CARTESIAN_POINT('Ctrl Pts',(1.60308384365138,2.12926487077458,-7.33498509220474));
#16675=CARTESIAN_POINT('Ctrl Pts',(1.61429177548598,2.11766008923023,-7.33724825699667));
#16676=CARTESIAN_POINT('Ctrl Pts',(1.62281870648737,2.10883123721941,-7.33897005994038));
#16677=CARTESIAN_POINT('Ctrl Pts',(1.63128633441429,2.09994067011115,-7.34069366478485));
#16678=CARTESIAN_POINT('Ctrl Pts',(1.63968819128585,2.09099554765498,-7.342417896705));
#16679=CARTESIAN_POINT('Ctrl Pts',(1.70117666231045,2.02553122097506,-7.35503658160788));
#16680=CARTESIAN_POINT('Ctrl Pts',(1.7592398126132,1.95705067552547,-7.36770770253109));
#16681=CARTESIAN_POINT('Ctrl Pts',(1.81371002961462,1.88587543597805,-7.38045292702293));
#16682=CARTESIAN_POINT('Ctrl Pts',(1.86796536455275,1.81498097890537,-7.39314787229272));
#16683=CARTESIAN_POINT('Ctrl Pts',(1.91865635294755,1.74141204884235,-7.40591633761525));
#16684=CARTESIAN_POINT('Ctrl Pts',(1.96556921350444,1.66546856046612,-7.41877973511718));
#16685=CARTESIAN_POINT('Ctrl Pts',(2.01167925042842,1.59082469923926,-7.43142300024196));
#16686=CARTESIAN_POINT('Ctrl Pts',(2.05413950023982,1.51388595667896,-7.44415797618339));
#16687=CARTESIAN_POINT('Ctrl Pts',(2.09269735617246,1.43493390097717,-7.45700499449054));
#16688=CARTESIAN_POINT('Ctrl Pts',(2.11347557683795,1.39238788290419,-7.46392805011235));
#16689=CARTESIAN_POINT('Ctrl Pts',(2.13311968690992,1.34925723096723,-7.4708836424134));
#16690=CARTESIAN_POINT('Ctrl Pts',(2.15158382290223,1.30558696879693,-7.47787495307664));
#16691=CARTESIAN_POINT('Ctrl Pts',(2.15703256236091,1.29269993846108,-7.4799380786025));
#16692=CARTESIAN_POINT('Ctrl Pts',(2.16237928721174,1.27976400868627,-7.48200462000068));
#16693=CARTESIAN_POINT('Ctrl Pts',(2.16762028210649,1.26678646608345,-7.48407368538072));
#16694=CARTESIAN_POINT('Ctrl Pts',(2.1995233363961,1.1877893950085,-7.4966685278627));
#16695=CARTESIAN_POINT('Ctrl Pts',(2.22741547616661,1.107495335724,-7.50931797811288));
#16696=CARTESIAN_POINT('Ctrl Pts',(2.25111999516359,1.02617308053887,-7.52204418386055));
#16697=CARTESIAN_POINT('Ctrl Pts',(2.27447329643854,0.94605573557442,-7.53458183193307));
#16698=CARTESIAN_POINT('Ctrl Pts',(2.29376221982233,0.864939616052927,-7.54719397785926));
#16699=CARTESIAN_POINT('Ctrl Pts',(2.30876812899223,0.783083312057354,-7.55990179942786));
#16700=CARTESIAN_POINT('Ctrl Pts',(2.32333320662229,0.703631716775364,-7.57223630082726));
#16701=CARTESIAN_POINT('Ctrl Pts',(2.3338631266181,0.623482150018367,-7.58466093907477));
#16702=CARTESIAN_POINT('Ctrl Pts',(2.34011118715382,0.542883112509629,-7.59719507982054));
#16703=CARTESIAN_POINT('Ctrl Pts',(2.34523285688384,0.476814346319474,-7.6074695848261));
#16704=CARTESIAN_POINT('Ctrl Pts',(2.34747653436054,0.410443624436012,-7.61781766931087));
#16705=CARTESIAN_POINT('Ctrl Pts',(2.34668236863854,0.343918483395443,-7.62825));
#16706=CARTESIAN_POINT('Ctrl Pts',(-2.54872116535053,-0.00229165091991107,
-7.45095259589208));
#16707=CARTESIAN_POINT('Ctrl Pts',(-2.54884325303734,-0.00474672992966245,
-7.45085547912962));
#16708=CARTESIAN_POINT('Ctrl Pts',(-2.54896183162798,-0.00720206634178606,
-7.45075836090064));
#16709=CARTESIAN_POINT('Ctrl Pts',(-2.54907689689922,-0.00965765243994136,
-7.45066124109941));
#16710=CARTESIAN_POINT('Ctrl Pts',(-2.55333516415932,-0.100532525222233,
-7.44706708914183));
#16711=CARTESIAN_POINT('Ctrl Pts',(-2.55276357918561,-0.191272512218256,
-7.4434895845571));
#16712=CARTESIAN_POINT('Ctrl Pts',(-2.54727379502897,-0.281480958790373,
-7.43992360795864));
#16713=CARTESIAN_POINT('Ctrl Pts',(-2.54185772847415,-0.370478073522051,
-7.43640551580072));
#16714=CARTESIAN_POINT('Ctrl Pts',(-2.53165485646165,-0.45895878699389,
-7.43289864410887));
#16715=CARTESIAN_POINT('Ctrl Pts',(-2.51653085824622,-0.546550786572665,
-7.42939807697118));
#16716=CARTESIAN_POINT('Ctrl Pts',(-2.51229227063912,-0.571098948944002,
-7.42841702286919));
#16717=CARTESIAN_POINT('Ctrl Pts',(-2.50766684965454,-0.595577313484347,
-7.42743646394764));
#16718=CARTESIAN_POINT('Ctrl Pts',(-2.50265089448421,-0.619977651269288,
-7.42645629199643));
#16719=CARTESIAN_POINT('Ctrl Pts',(-2.48482398915618,-0.706697427840933,
-7.42297272167212));
#16720=CARTESIAN_POINT('Ctrl Pts',(-2.46206809920096,-0.792432697411164,
-7.41949403924777));
#16721=CARTESIAN_POINT('Ctrl Pts',(-2.43465304171894,-0.87692613469852,
-7.41601538697891));
#16722=CARTESIAN_POINT('Ctrl Pts',(-2.42548539819617,-0.905180888990806,
-7.41485211953139));
#16723=CARTESIAN_POINT('Ctrl Pts',(-2.41579632851701,-0.933296653750345,
-7.413688855456));
#16724=CARTESIAN_POINT('Ctrl Pts',(-2.40559471855271,-0.961263367130259,
-7.41252541310066));
#16725=CARTESIAN_POINT('Ctrl Pts',(-2.39903093632121,-0.979257332494453,
-7.41177684671888));
#16726=CARTESIAN_POINT('Ctrl Pts',(-2.39225293451855,-0.9971944580043,-7.41102800099647));
#16727=CARTESIAN_POINT('Ctrl Pts',(-2.385274720724,-1.0150428927436,-7.41028005192424));
#16728=CARTESIAN_POINT('Ctrl Pts',(-2.35172893850088,-1.10084417691406,
-7.40668449904645));
#16729=CARTESIAN_POINT('Ctrl Pts',(-2.3135230946086,-1.18470956672032,-7.40310499394341));
#16730=CARTESIAN_POINT('Ctrl Pts',(-2.27102243831346,-1.26637331179736,
-7.39953639877998));
#16731=CARTESIAN_POINT('Ctrl Pts',(-2.22895234350611,-1.34720974580101,
-7.39600395599104));
#16732=CARTESIAN_POINT('Ctrl Pts',(-2.1826732982571,-1.425889649158,-7.39248220321072));
#16733=CARTESIAN_POINT('Ctrl Pts',(-2.13248447954121,-1.50214210424881,
-7.38896615717692));
#16734=CARTESIAN_POINT('Ctrl Pts',(-2.08204495359797,-1.57877546174146,
-7.38543254750694));
#16735=CARTESIAN_POINT('Ctrl Pts',(-2.0276559274001,-1.65295784872659,-7.38190470173949));
#16736=CARTESIAN_POINT('Ctrl Pts',(-1.96957457655766,-1.72438946587683,
-7.37837756156043));
#16737=CARTESIAN_POINT('Ctrl Pts',(-1.94762706422866,-1.75138171511597,
-7.37704474213659));
#16738=CARTESIAN_POINT('Ctrl Pts',(-1.92515189733108,-1.77798086862864,
-7.37571202346358));
#16739=CARTESIAN_POINT('Ctrl Pts',(-1.90216149454643,-1.80416947090812,
-7.3743791326112));
#16740=CARTESIAN_POINT('Ctrl Pts',(-1.88977962052994,-1.81827378987677,
-7.37366128148147));
#16741=CARTESIAN_POINT('Ctrl Pts',(-1.87724828731966,-1.83225901324112,
-7.37294338041035));
#16742=CARTESIAN_POINT('Ctrl Pts',(-1.86456935020798,-1.8461223147433,-7.37222538676236));
#16743=CARTESIAN_POINT('Ctrl Pts',(-1.85494278415337,-1.85664811721949,
-7.37168024538196));
#16744=CARTESIAN_POINT('Ctrl Pts',(-1.84523713445571,-1.86709703864532,
-7.37113539153293));
#16745=CARTESIAN_POINT('Ctrl Pts',(-1.83545598652633,-1.87746553404443,
-7.37059094249616));
#16746=CARTESIAN_POINT('Ctrl Pts',(-1.77171523636253,-1.94503384806859,
-7.36704293460588));
#16747=CARTESIAN_POINT('Ctrl Pts',(-1.70473932291081,-2.00922447566438,
-7.36351026093116));
#16748=CARTESIAN_POINT('Ctrl Pts',(-1.63483249771768,-2.0697661447767,-7.35998798155957));
#16749=CARTESIAN_POINT('Ctrl Pts',(-1.56489051873596,-2.13033825825596,
-7.35646393095228));
#16750=CARTESIAN_POINT('Ctrl Pts',(-1.49201405105733,-2.18725850548537,
-7.35295028510463));
#16751=CARTESIAN_POINT('Ctrl Pts',(-1.41646639948432,-2.24022488946181,
-7.3494420966481));
#16752=CARTESIAN_POINT('Ctrl Pts',(-1.34208268676144,-2.29237523705884,
-7.34598795774511));
#16753=CARTESIAN_POINT('Ctrl Pts',(-1.26510879589927,-2.34069325196222,
-7.34253910936801));
#16754=CARTESIAN_POINT('Ctrl Pts',(-1.18576568003122,-2.38485106755256,
-7.33909082931102));
#16755=CARTESIAN_POINT('Ctrl Pts',(-1.15640740682169,-2.40119019414539,
-7.33781490830756));
#16756=CARTESIAN_POINT('Ctrl Pts',(-1.12672450477203,-2.41695929561798,
-7.33653906511412));
#16757=CARTESIAN_POINT('Ctrl Pts',(-1.09672736577269,-2.43214008652495,
-7.33526306050453));
#16758=CARTESIAN_POINT('Ctrl Pts',(-1.08062679344899,-2.44028817764571,
-7.3345781817065));
#16759=CARTESIAN_POINT('Ctrl Pts',(-1.06443568717334,-2.448266767796,-7.33389325640666));
#16760=CARTESIAN_POINT('Ctrl Pts',(-1.04815561213944,-2.45607290918114,
-7.33320824761425));
#16761=CARTESIAN_POINT('Ctrl Pts',(-1.0370323350443,-2.46140641492298,-7.33274021889849));
#16762=CARTESIAN_POINT('Ctrl Pts',(-1.02586911010053,-2.4666586051756,-7.33227221874498));
#16763=CARTESIAN_POINT('Ctrl Pts',(-1.01467488717969,-2.47182484947527,
-7.3318045847467));
#16764=CARTESIAN_POINT('Ctrl Pts',(-0.964722922882861,-2.49487817373284,
-7.32971786225141));
#16765=CARTESIAN_POINT('Ctrl Pts',(-0.91410779186745,-2.51624284380486,
-7.32763648114457));
#16766=CARTESIAN_POINT('Ctrl Pts',(-0.8628861291915,-2.53585963668761,-7.32555943799463));
#16767=CARTESIAN_POINT('Ctrl Pts',(-0.779322982596467,-2.56786252089221,
-7.32217094468622));
#16768=CARTESIAN_POINT('Ctrl Pts',(-0.694146848480023,-2.59521630651244,
-7.31879399673727));
#16769=CARTESIAN_POINT('Ctrl Pts',(-0.607724558635994,-2.61805914565455,
-7.31542423731298));
#16770=CARTESIAN_POINT('Ctrl Pts',(-0.519092379891881,-2.64148609494646,
-7.31196831037378));
#16771=CARTESIAN_POINT('Ctrl Pts',(-0.429148743139305,-2.66016857380842,
-7.30851994429254));
#16772=CARTESIAN_POINT('Ctrl Pts',(-0.338268208316806,-2.6742053818501,
-7.30507443939171));
#16773=CARTESIAN_POINT('Ctrl Pts',(-0.248676928654702,-2.68804306004249,
-7.30167781332925));
#16774=CARTESIAN_POINT('Ctrl Pts',(-0.158174285448021,-2.69736576180666,
-7.29828396784411));
#16775=CARTESIAN_POINT('Ctrl Pts',(-0.0671111582030917,-2.70222088552231,
-7.2948884004473));
#16776=CARTESIAN_POINT('Ctrl Pts',(-0.045603233936238,-2.70336760249044,
-7.29408641166629));
#16777=CARTESIAN_POINT('Ctrl Pts',(-0.0240569840929646,-2.70426498015991,
-7.29328406477781));
#16778=CARTESIAN_POINT('Ctrl Pts',(-0.00251467253543246,-2.70491251705096,
-7.29248269889014));
#16779=CARTESIAN_POINT('Ctrl Pts',(0.0913505575722242,-2.70773399696131,
-7.28899094763375));
#16780=CARTESIAN_POINT('Ctrl Pts',(0.185240927263786,-2.7058247172191,-7.28551403200604));
#16781=CARTESIAN_POINT('Ctrl Pts',(0.278764535523396,-2.69931752457491,
-7.28204725167995));
#16782=CARTESIAN_POINT('Ctrl Pts',(0.373533208232459,-2.69272370274288,
-7.27853431867628));
#16783=CARTESIAN_POINT('Ctrl Pts',(0.467926227188296,-2.68140873303817,
-7.27503179262975));
#16784=CARTESIAN_POINT('Ctrl Pts',(0.561545441819487,-2.66545794439719,
-7.27153478297901));
#16785=CARTESIAN_POINT('Ctrl Pts',(0.654945657927808,-2.64954446860021,
-7.26804595369969));
#16786=CARTESIAN_POINT('Ctrl Pts',(0.747576659440711,-2.62901672313918,
-7.26456261503792));
#16787=CARTESIAN_POINT('Ctrl Pts',(0.839038170974715,-2.60390818657947,
-7.26107991067285));
#16788=CARTESIAN_POINT('Ctrl Pts',(0.879163798785432,-2.59289267004177,
-7.25955199257064));
#16789=CARTESIAN_POINT('Ctrl Pts',(0.919064181798801,-2.58099482605824,
-7.25802419655261));
#16790=CARTESIAN_POINT('Ctrl Pts',(0.9587044796514,-2.56821443729529,-7.25649611254898));
#16791=CARTESIAN_POINT('Ctrl Pts',(0.977255688629643,-2.56223336057265,
-7.25578098659828));
#16792=CARTESIAN_POINT('Ctrl Pts',(0.995749923609562,-2.55605896850107,
-7.25506579757489));
#16793=CARTESIAN_POINT('Ctrl Pts',(1.01418354344848,-2.54969110077333,-7.25435050344838));
#16794=CARTESIAN_POINT('Ctrl Pts',(1.0270766997497,-2.54523717828622,-7.25385020024938));
#16795=CARTESIAN_POINT('Ctrl Pts',(1.03993108370967,-2.54069175052625,-7.25335019936401));
#16796=CARTESIAN_POINT('Ctrl Pts',(1.05274516772751,-2.53605528929552,-7.2528505022789));
#16797=CARTESIAN_POINT('Ctrl Pts',(1.14311406147389,-2.50335752707269,-7.24932648349403));
#16798=CARTESIAN_POINT('Ctrl Pts',(1.23148546628133,-2.46613421062177,-7.24581732198645));
#16799=CARTESIAN_POINT('Ctrl Pts',(1.31746058766075,-2.42447327586601,-7.24231818331382));
#16800=CARTESIAN_POINT('Ctrl Pts',(1.40202683996985,-2.38349503630713,-7.2388763848132));
#16801=CARTESIAN_POINT('Ctrl Pts',(1.48427560644325,-2.33822317751169,-7.23544428335181));
#16802=CARTESIAN_POINT('Ctrl Pts',(1.56381530896657,-2.28869332060664,-7.2320172782791));
#16803=CARTESIAN_POINT('Ctrl Pts',(1.62076292161253,-2.25323169558218,-7.22956366390508));
#16804=CARTESIAN_POINT('Ctrl Pts',(1.676321640262,-2.21558640461195,-7.22711266196708));
#16805=CARTESIAN_POINT('Ctrl Pts',(1.7303399838677,-2.17575595906912,-7.22466258399285));
#16806=CARTESIAN_POINT('Ctrl Pts',(1.77747898896718,-2.14099799630627,-7.22252452809531));
#16807=CARTESIAN_POINT('Ctrl Pts',(1.82344488788193,-2.10457574306011,-7.22038717580978));
#16808=CARTESIAN_POINT('Ctrl Pts',(1.86820503283264,-2.06657448017728,-7.21824940508842));
#16809=CARTESIAN_POINT('Ctrl Pts',(1.8902908163544,-2.04782369939881,-7.21719457514041));
#16810=CARTESIAN_POINT('Ctrl Pts',(1.9120829551215,-2.02868838834088,-7.21613964331649));
#16811=CARTESIAN_POINT('Ctrl Pts',(1.93357702544331,-2.0091783017074,-7.21508447482116));
#16812=CARTESIAN_POINT('Ctrl Pts',(1.94403188955915,-1.99968846094725,-7.21457123358427));
#16813=CARTESIAN_POINT('Ctrl Pts',(1.95440865049196,-1.99011682212725,-7.214058308234));
#16814=CARTESIAN_POINT('Ctrl Pts',(1.96470674377952,-1.98046518688763,-7.21354570043154));
#16815=CARTESIAN_POINT('Ctrl Pts',(2.03231051209255,-1.91710521389451,-7.21018059019757));
#16816=CARTESIAN_POINT('Ctrl Pts',(2.09653100691307,-1.85029719530032,-7.20682892803937));
#16817=CARTESIAN_POINT('Ctrl Pts',(2.15728945535032,-1.78043655567924,-7.2034865054898));
#16818=CARTESIAN_POINT('Ctrl Pts',(2.22026134829767,-1.70803087659091,-7.20002231770374));
#16819=CARTESIAN_POINT('Ctrl Pts',(2.27951493325531,-1.63234557769656,-7.19656805499097));
#16820=CARTESIAN_POINT('Ctrl Pts',(2.33492983764645,-1.55377538415515,-7.19311903197858));
#16821=CARTESIAN_POINT('Ctrl Pts',(2.38183708392325,-1.48726779997799,-7.19019952550943));
#16822=CARTESIAN_POINT('Ctrl Pts',(2.42599342603758,-1.41869208607858,-7.18728377337642));
#16823=CARTESIAN_POINT('Ctrl Pts',(2.4673039324097,-1.34826833541749,-7.18436893384037));
#16824=CARTESIAN_POINT('Ctrl Pts',(2.50345062548531,-1.28664755358903,-7.18181844924633));
#16825=CARTESIAN_POINT('Ctrl Pts',(2.53741825419599,-1.22361145783562,-7.17926866335933));
#16826=CARTESIAN_POINT('Ctrl Pts',(2.5691287863742,-1.15929983468204,-7.17671767243616));
#16827=CARTESIAN_POINT('Ctrl Pts',(2.57735307324704,-1.14262029000899,-7.17605606004049));
#16828=CARTESIAN_POINT('Ctrl Pts',(2.58542693226734,-1.12585155808721,-7.17539423637559));
#16829=CARTESIAN_POINT('Ctrl Pts',(2.5933377461211,-1.10902032020036,-7.17473311722116));
#16830=CARTESIAN_POINT('Ctrl Pts',(2.6349885962116,-1.02040296944197,-7.17125229017833));
#16831=CARTESIAN_POINT('Ctrl Pts',(2.67218718831404,-0.929929724788019,
-7.1677859564656));
#16832=CARTESIAN_POINT('Ctrl Pts',(2.70481573622773,-0.838000353098113,
-7.16432946488494));
#16833=CARTESIAN_POINT('Ctrl Pts',(2.73755084161654,-0.745770760823376,
-7.1608616851827));
#16834=CARTESIAN_POINT('Ctrl Pts',(2.76568644862227,-0.652074656152445,
-7.15740381200185));
#16835=CARTESIAN_POINT('Ctrl Pts',(2.78906022130522,-0.557287603626856,
-7.15395114842608));
#16836=CARTESIAN_POINT('Ctrl Pts',(2.81210271895143,-0.463843962142935,
-7.15054741923795));
#16837=CARTESIAN_POINT('Ctrl Pts',(2.83051771268829,-0.369339210646432,
-7.14714875303053));
#16838=CARTESIAN_POINT('Ctrl Pts',(2.84410218393759,-0.27411879745952,-7.14375064977776));
#16839=CARTESIAN_POINT('Ctrl Pts',(2.85077740762626,-0.227328786565033,
-7.14208086823727));
#16840=CARTESIAN_POINT('Ctrl Pts',(2.85628549214726,-0.180365830909598,
-7.14041122262811));
#16841=CARTESIAN_POINT('Ctrl Pts',(2.860597698937,-0.133270579992977,-7.13874117902033));
#16842=CARTESIAN_POINT('Ctrl Pts',(2.86229734993567,-0.114708044809467,
-7.13808293338783));
#16843=CARTESIAN_POINT('Ctrl Pts',(2.86381118226309,-0.0961249578213986,
-7.13742462592495));
#16844=CARTESIAN_POINT('Ctrl Pts',(2.86513729621133,-0.0775238157094563,
-7.13676622393794));
#16845=CARTESIAN_POINT('Ctrl Pts',(2.86615128521417,-0.0633007894251151,
-7.13626278878806));
#16846=CARTESIAN_POINT('Ctrl Pts',(2.86705513484125,-0.0490720314096428,
-7.13575946921485));
#16847=CARTESIAN_POINT('Ctrl Pts',(2.86784786602706,-0.034846719776545,
-7.13525653467227));
#16848=CARTESIAN_POINT('Ctrl Pts',(2.87331995000557,0.0633481049887041,
-7.1317848659629));
#16849=CARTESIAN_POINT('Ctrl Pts',(2.87350981423829,0.161493285384653,-7.12832744179556));
#16850=CARTESIAN_POINT('Ctrl Pts',(2.86825916071671,0.259214272665054,-7.12487964669447));
#16851=CARTESIAN_POINT('Ctrl Pts',(2.86769353153745,0.26974131308102,-7.12450823130679));
#16852=CARTESIAN_POINT('Ctrl Pts',(2.86706471810811,0.280263443667678,-7.12413692766231));
#16853=CARTESIAN_POINT('Ctrl Pts',(2.86637248699574,0.290780204225716,-7.12376572999106));
#16854=CARTESIAN_POINT('Ctrl Pts',(2.86009088031278,0.386213871138418,-7.12039732061053));
#16855=CARTESIAN_POINT('Ctrl Pts',(2.8485916250155,0.481205266105106,-7.11703763763718));
#16856=CARTESIAN_POINT('Ctrl Pts',(2.83214991077614,0.57546107308452,-7.11368236954826));
#16857=CARTESIAN_POINT('Ctrl Pts',(2.8153985065753,0.671492247085209,-7.11026390288831));
#16858=CARTESIAN_POINT('Ctrl Pts',(2.79351642813581,0.766760638665728,-7.10685001899331));
#16859=CARTESIAN_POINT('Ctrl Pts',(2.76674040525016,0.860950212594716,-7.10343615809206));
#16860=CARTESIAN_POINT('Ctrl Pts',(2.75761693499742,0.89304369337525,-7.10227294358061));
#16861=CARTESIAN_POINT('Ctrl Pts',(2.74792484490626,0.92501182174776,-7.10110973173872));
#16862=CARTESIAN_POINT('Ctrl Pts',(2.73767218810561,0.956841690536304,-7.09994634218776));
#16863=CARTESIAN_POINT('Ctrl Pts',(2.73046159724209,0.97922731852874,-7.09912814196611));
#16864=CARTESIAN_POINT('Ctrl Pts',(2.72297372710465,1.00154455613911,-7.09830985384657));
#16865=CARTESIAN_POINT('Ctrl Pts',(2.71521119495974,1.0237888281201,-7.09749141508282));
#16866=CARTESIAN_POINT('Ctrl Pts',(2.7105158736684,1.03724371653708,-7.09699636618881));
#16867=CARTESIAN_POINT('Ctrl Pts',(2.70572160653792,1.05066736008874,-7.09650142908722));
#16868=CARTESIAN_POINT('Ctrl Pts',(2.70083194831629,1.06405145610732,-7.09600686216269));
#16869=CARTESIAN_POINT('Ctrl Pts',(2.666977201111,1.15671952547791,-7.09258260683707));
#16870=CARTESIAN_POINT('Ctrl Pts',(2.62851664991674,1.24759973569772,-7.08917213696652));
#16871=CARTESIAN_POINT('Ctrl Pts',(2.58574587816133,1.33638733434256,-7.08577102509522));
#16872=CARTESIAN_POINT('Ctrl Pts',(2.54241251743573,1.426342808189,-7.08232517641075));
#16873=CARTESIAN_POINT('Ctrl Pts',(2.49465442167471,1.5141510805358,-7.07888893352709));
#16874=CARTESIAN_POINT('Ctrl Pts',(2.44272590781198,1.59948420693675,-7.07545769196954));
#16875=CARTESIAN_POINT('Ctrl Pts',(2.39086769403728,1.68470181055743,-7.0720310955783));
#16876=CARTESIAN_POINT('Ctrl Pts',(2.33484985166447,1.76745178247923,-7.06860948698087));
#16877=CARTESIAN_POINT('Ctrl Pts',(2.27487983880247,1.84738429843036,-7.06518828037767));
#16878=CARTESIAN_POINT('Ctrl Pts',(2.23288468478585,1.90335857887663,-7.06279251470467));
#16879=CARTESIAN_POINT('Ctrl Pts',(2.18895051670804,1.95795077859895,-7.06039694616037));
#16880=CARTESIAN_POINT('Ctrl Pts',(2.14313711407334,2.01103068470338,-7.058));
#16881=CARTESIAN_POINT('Ctrl Pts',(0.545102916878531,2.89105980740809,-7.95748399100539));
#16882=CARTESIAN_POINT('Ctrl Pts',(-0.418551816366991,3.07275477082944,
-7.90443409773202));
#16883=CARTESIAN_POINT('Ctrl Pts',(-2.52507517261166,2.39323450065356,-7.79833431118528));
#16884=CARTESIAN_POINT('Ctrl Pts',(-3.38010884006162,-0.837958625187954,
-7.63918463136517));
#16885=CARTESIAN_POINT('Ctrl Pts',(-1.12023390429596,-3.29384205719836,
-7.48003495154506));
#16886=CARTESIAN_POINT('Ctrl Pts',(2.16577264269164,-2.72400316663615,-7.32088527172496));
#16887=CARTESIAN_POINT('Ctrl Pts',(3.4626380957396,0.351377294665846,-7.16173559190485));
#16888=CARTESIAN_POINT('Ctrl Pts',(1.57515132522855,3.10306773376032,-7.00258591208474));
#16889=CARTESIAN_POINT('Ctrl Pts',(-1.75990653256836,3.00232659448819,-6.84343623226463));
#16890=CARTESIAN_POINT('Ctrl Pts',(-3.47728821638593,0.141248766687278,
-6.68428655244452));
#16891=CARTESIAN_POINT('Ctrl Pts',(-1.99771660476884,-2.84959140114192,
-6.52513687262442));
#16892=CARTESIAN_POINT('Ctrl Pts',(1.3183600049385,-3.22073768325123,-6.3659871928043));
#16893=CARTESIAN_POINT('Ctrl Pts',(3.42245518605895,-0.630906395973156,
-6.20683751298421));
#16894=CARTESIAN_POINT('Ctrl Pts',(2.38013079602577,2.53892891859366,-6.04768783316409));
#16895=CARTESIAN_POINT('Ctrl Pts',(-0.850331682068317,3.37463293930467,
-5.88853815334399));
#16896=CARTESIAN_POINT('Ctrl Pts',(-3.29905605961118,1.10789918584346,-5.72938847352388));
#16897=CARTESIAN_POINT('Ctrl Pts',(-2.71482419166764,-2.17736841611413,
-5.57023879370378));
#16898=CARTESIAN_POINT('Ctrl Pts',(0.365251897578816,-3.46089570740757,
-5.41108911388365));
#16899=CARTESIAN_POINT('Ctrl Pts',(3.10953820283011,-1.56268354366004,-5.25193943406356));
#16900=CARTESIAN_POINT('Ctrl Pts',(2.9951020675602,1.77216542315489,-5.09278975424344));
#16901=CARTESIAN_POINT('Ctrl Pts',(0.127149812658285,3.47779244265733,-4.93364007442334));
#16902=CARTESIAN_POINT('Ctrl Pts',(-2.85769643090647,1.9861466101059,-4.77449039460323));
#16903=CARTESIAN_POINT('Ctrl Pts',(-3.21534873908604,-1.3314426796523,-4.61534071478312));
#16904=CARTESIAN_POINT('Ctrl Pts',(-0.617003224446478,-3.42498383104617,
-4.45619103496301));
#16905=CARTESIAN_POINT('Ctrl Pts',(2.54857788636968,-2.36980124815908,-4.29704135514291));
#16906=CARTESIAN_POINT('Ctrl Pts',(3.371150073419,0.864033777125352,-4.1378916753228));
#16907=CARTESIAN_POINT('Ctrl Pts',(1.09449005337646,3.30352822398509,-3.97874199550269));
#16908=CARTESIAN_POINT('Ctrl Pts',(-2.1883781623069,2.70595790881245,-3.81959231568258));
#16909=CARTESIAN_POINT('Ctrl Pts',(-3.45938338148725,-0.379307024135721,
-3.66044263586248));
#16910=CARTESIAN_POINT('Ctrl Pts',(-1.55004000081492,-3.11585994835756,
-3.50129295604237));
#16911=CARTESIAN_POINT('Ctrl Pts',(1.78431673513788,-2.98787899886338,-3.34214327622227));
#16912=CARTESIAN_POINT('Ctrl Pts',(3.47828021156799,-0.113022200762772,
-3.18299359640215));
#16913=CARTESIAN_POINT('Ctrl Pts',(1.97452245968913,2.86574046369287,-3.02384391658205));
#16914=CARTESIAN_POINT('Ctrl Pts',(-1.34449219737245,3.20991392615656,-2.86469423676194));
#16915=CARTESIAN_POINT('Ctrl Pts',(-3.42746184614662,0.603086217463922,
-2.70554455694183));
#16916=CARTESIAN_POINT('Ctrl Pts',(-2.35942946044921,-2.55818307933608,
-2.54639487712173));
#16917=CARTESIAN_POINT('Ctrl Pts',(0.877719845461013,-3.36761213384782,
-2.38724519730161));
#16918=CARTESIAN_POINT('Ctrl Pts',(3.30794705758641,-1.08106325192158,-2.22809551748151));
#16919=CARTESIAN_POINT('Ctrl Pts',(2.69704588622583,2.19935329862247,-2.0689458376614));
#16920=CARTESIAN_POINT('Ctrl Pts',(-0.393354403714323,3.45781071965196,
-1.90979615784129));
#16921=CARTESIAN_POINT('Ctrl Pts',(-3.12213281863858,1.53737732643667,-1.75064647802119));
#16922=CARTESIAN_POINT('Ctrl Pts',(-2.98060194491491,-1.79645104940419,
-1.59149679820108));
#16923=CARTESIAN_POINT('Ctrl Pts',(-0.0989016115630054,-3.47868671450324,
-1.43234711838097));
#16924=CARTESIAN_POINT('Ctrl Pts',(2.87375418364955,-1.96291147173372,-1.27319743856086));
#16925=CARTESIAN_POINT('Ctrl Pts',(3.20439368630738,1.35760711787367,-1.11404775874076));
#16926=CARTESIAN_POINT('Ctrl Pts',(0.58922140315462,3.42971561441151,-0.954898078920646));
#16927=CARTESIAN_POINT('Ctrl Pts',(-2.56786503715982,2.34933985115096,-0.795748399100539));
#16928=CARTESIAN_POINT('Ctrl Pts',(-3.36379079604088,-0.89200665476552,
-0.636598719280432));
#16929=CARTESIAN_POINT('Ctrl Pts',(-1.06805538932566,-3.31112929125929,
-0.477449039460324));
#16930=CARTESIAN_POINT('Ctrl Pts',(2.21113366938903,-2.69038999483046,-0.318299359640216));
#16931=CARTESIAN_POINT('Ctrl Pts',(3.45452145423158,0.412137749680903,-0.159149679820109));
#16932=CARTESIAN_POINT('Ctrl Pts',(2.17043456109762,2.21499916944277,-0.0530498932733694));
#16933=CARTESIAN_POINT('Ctrl Pts',(1.28892185405323,2.64462557919718,0.));
#16934=CARTESIAN_POINT('Ctrl Pts',(0.509883685250385,2.70426773226936,-7.84773932733692));
#16935=CARTESIAN_POINT('Ctrl Pts',(-0.391509082027172,2.8742233400493,-7.79468943406355));
#16936=CARTESIAN_POINT('Ctrl Pts',(-2.36192945346575,2.23860703928967,-7.68858964751681));
#16937=CARTESIAN_POINT('Ctrl Pts',(-3.16171918834565,-0.783817915238558,
-7.52943996769672));
#16938=CARTESIAN_POINT('Ctrl Pts',(-1.04785532012138,-3.0810261232399,-7.37029028787659));
#16939=CARTESIAN_POINT('Ctrl Pts',(2.02584154712231,-2.54800466156315,-7.2111406080565));
#16940=CARTESIAN_POINT('Ctrl Pts',(3.23891620880379,0.32867472246064,-7.05199092823639));
#16941=CARTESIAN_POINT('Ctrl Pts',(1.47338041618576,2.90257777509537,-6.89284124841627));
#16942=CARTESIAN_POINT('Ctrl Pts',(-1.64619854478261,2.80834554525786,-6.73369156859618));
#16943=CARTESIAN_POINT('Ctrl Pts',(-3.25261978160301,0.132122649623666,
-6.57454188877606));
#16944=CARTESIAN_POINT('Ctrl Pts',(-1.86864365055748,-2.66547860978671,
-6.41539220895596));
#16945=CARTESIAN_POINT('Ctrl Pts',(1.23318044536269,-3.01264504061877,-6.25624252913584));
#16946=CARTESIAN_POINT('Ctrl Pts',(3.20132952666057,-0.590143380756329,
-6.09709284931574));
#16947=CARTESIAN_POINT('Ctrl Pts',(2.22634996819508,2.3748881055608,-5.93794316949563));
#16948=CARTESIAN_POINT('Ctrl Pts',(-0.795391545913839,3.15659708686432,
-5.77879348967553));
#16949=CARTESIAN_POINT('Ctrl Pts',(-3.08590324769261,1.03631755081884,-5.61964380985541));
#16950=CARTESIAN_POINT('Ctrl Pts',(-2.53941874239294,-2.0366881148124,-5.46049413003531));
#16951=CARTESIAN_POINT('Ctrl Pts',(0.34165288391529,-3.23728639660436,-5.3013444502152));
#16952=CARTESIAN_POINT('Ctrl Pts',(2.9086301855897,-1.4617181810074,-5.1421947703951));
#16953=CARTESIAN_POINT('Ctrl Pts',(2.80158779676639,1.65766538547598,-4.98304509057499));
#16954=CARTESIAN_POINT('Ctrl Pts',(0.118934632432992,3.25309142969275,-4.82389541075487));
#16955=CARTESIAN_POINT('Ctrl Pts',(-2.67305997161298,1.85782119605504,-4.66474573093477));
#16956=CARTESIAN_POINT('Ctrl Pts',(-3.00760427744274,-1.24541784529113,
-4.50559605111466));
#16957=CARTESIAN_POINT('Ctrl Pts',(-0.577138496513027,-3.20369479528205,
-4.34644637129456));
#16958=CARTESIAN_POINT('Ctrl Pts',(2.38391365118927,-2.21668781492061,-4.18729669147445));
#16959=CARTESIAN_POINT('Ctrl Pts',(3.153339249788,0.808208345286956,-4.02814701165434));
#16960=CARTESIAN_POINT('Ctrl Pts',(1.02377478565178,3.09008646444198,-3.86899733183423));
#16961=CARTESIAN_POINT('Ctrl Pts',(-2.04698651863418,2.53112531222279,-3.70984765201412));
#16962=CARTESIAN_POINT('Ctrl Pts',(-3.23587178242843,-0.354799905337474,
-3.55069797219402));
#16963=CARTESIAN_POINT('Ctrl Pts',(-1.44989154053112,-2.91454348160582,
-3.39154829237391));
#16964=CARTESIAN_POINT('Ctrl Pts',(1.66903159824548,-2.79483141228941,-3.2323986125538));
#16965=CARTESIAN_POINT('Ctrl Pts',(3.25354768373583,-0.105719808967507,
-3.0732489327337));
#16966=CARTESIAN_POINT('Ctrl Pts',(1.84694808481515,2.68058427749065,-2.91409925291358));
#16967=CARTESIAN_POINT('Ctrl Pts',(-1.25762423050732,3.00252060909438,-2.75494957309348));
#16968=CARTESIAN_POINT('Ctrl Pts',(-3.20601270522604,0.564120670726008,
-2.59579989327337));
#16969=CARTESIAN_POINT('Ctrl Pts',(-2.20698615092947,-2.39289825030919,
-2.43665021345326));
#16970=CARTESIAN_POINT('Ctrl Pts',(0.82101015342905,-3.15002989735035,-2.27750053363316));
#16971=CARTESIAN_POINT('Ctrl Pts',(3.0942197961329,-1.01121549309444,-2.11835085381304));
#16972=CARTESIAN_POINT('Ctrl Pts',(2.52278909757635,2.05725254873131,-1.95920117399294));
#16973=CARTESIAN_POINT('Ctrl Pts',(-0.367939680315494,3.23440073065564,
-1.80005149417283));
#16974=CARTESIAN_POINT('Ctrl Pts',(-2.92041106021703,1.43804700461472,-1.64090181435273));
#16975=CARTESIAN_POINT('Ctrl Pts',(-2.78802453056098,-1.68038191152489,
-1.48175213453262));
#16976=CARTESIAN_POINT('Ctrl Pts',(-0.0925115544596916,-3.25392792241787,
-1.32260245471251));
#16977=CARTESIAN_POINT('Ctrl Pts',(2.68808022905787,-1.8360872856068,-1.1634527748924));
#16978=CARTESIAN_POINT('Ctrl Pts',(2.99735703328033,1.26989179281504,-1.00430309507229));
#16979=CARTESIAN_POINT('Ctrl Pts',(0.551151665430965,3.20812085697687,-0.845153415252187));
#16980=CARTESIAN_POINT('Ctrl Pts',(-2.4019546544904,2.19754843373437,-0.686003735432076));
#16981=CARTESIAN_POINT('Ctrl Pts',(-3.14645545710565,-0.834373888520336,
-0.526854055611971));
#16982=CARTESIAN_POINT('Ctrl Pts',(-0.9990480716548,-3.0971964249166,-0.367704375791862));
#16983=CARTESIAN_POINT('Ctrl Pts',(2.0682717868863,-2.51656324493786,-0.208554695971755));
#16984=CARTESIAN_POINT('Ctrl Pts',(3.23132398547161,0.385509429744861,-0.049405016151647));
#16985=CARTESIAN_POINT('Ctrl Pts',(2.03020225784972,2.07188753604432,0.0566947703950921));
#16986=CARTESIAN_POINT('Ctrl Pts',(1.20564430054384,2.47375567929493,0.109744663668461));
#16987=CARTESIAN_POINT('Ctrl Pts',(0.474664453622239,2.51747565713063,-7.73799466366846));
#16988=CARTESIAN_POINT('Ctrl Pts',(-0.364466347687353,2.67569190926916,
-7.6849447703951));
#16989=CARTESIAN_POINT('Ctrl Pts',(-2.19878373431984,2.08397957792578,-7.57884498384835));
#16990=CARTESIAN_POINT('Ctrl Pts',(-2.94332953662968,-0.729677205289159,
-7.41969530402826));
#16991=CARTESIAN_POINT('Ctrl Pts',(-0.975476735946805,-2.86821018928144,
-7.26054562420813));
#16992=CARTESIAN_POINT('Ctrl Pts',(1.88591045155299,-2.37200615649015,-7.10139594438804));
#16993=CARTESIAN_POINT('Ctrl Pts',(3.01519432186797,0.305972150255433,-6.94224626456792));
#16994=CARTESIAN_POINT('Ctrl Pts',(1.37160950714298,2.70208781643043,-6.78309658474782));
#16995=CARTESIAN_POINT('Ctrl Pts',(-1.53249055699685,2.61436449602753,-6.62394690492771));
#16996=CARTESIAN_POINT('Ctrl Pts',(-3.02795134682008,0.12299653256005,-6.4647972251076));
#16997=CARTESIAN_POINT('Ctrl Pts',(-1.73957069634612,-2.48136581843149,
-6.3056475452875));
#16998=CARTESIAN_POINT('Ctrl Pts',(1.14800088578687,-2.80455239798632,-6.14649786546738));
#16999=CARTESIAN_POINT('Ctrl Pts',(2.98020386726219,-0.549380365539499,
-5.98734818564728));
#17000=CARTESIAN_POINT('Ctrl Pts',(2.07256914036438,2.21084729252794,-5.82819850582717));
#17001=CARTESIAN_POINT('Ctrl Pts',(-0.740451409759363,2.93856123442398,
-5.66904882600706));
#17002=CARTESIAN_POINT('Ctrl Pts',(-2.87275043577405,0.964735915794223,
-5.50989914618696));
#17003=CARTESIAN_POINT('Ctrl Pts',(-2.36401329311824,-1.89600781351067,
-5.35074946636685));
#17004=CARTESIAN_POINT('Ctrl Pts',(0.318053870251765,-3.01367708580114,
-5.19159978654674));
#17005=CARTESIAN_POINT('Ctrl Pts',(2.70772216834929,-1.36075281835476,-5.03245010672663));
#17006=CARTESIAN_POINT('Ctrl Pts',(2.60807352597257,1.54316534779707,-4.87330042690653));
#17007=CARTESIAN_POINT('Ctrl Pts',(0.1107194522077,3.02839041672818,-4.71415074708642));
#17008=CARTESIAN_POINT('Ctrl Pts',(-2.48842351231948,1.72949578200417,-4.55500106726631));
#17009=CARTESIAN_POINT('Ctrl Pts',(-2.79985981579943,-1.15939301092996,
-4.3958513874462));
#17010=CARTESIAN_POINT('Ctrl Pts',(-0.537273768579575,-2.98240575951794,
-4.23670170762609));
#17011=CARTESIAN_POINT('Ctrl Pts',(2.21924941600886,-2.06357438168214,-4.07755202780599));
#17012=CARTESIAN_POINT('Ctrl Pts',(2.935528426157,0.752382913448559,-3.91840234798588));
#17013=CARTESIAN_POINT('Ctrl Pts',(0.953059517927111,2.87664470489887,-3.75925266816577));
#17014=CARTESIAN_POINT('Ctrl Pts',(-1.90559487496145,2.35629271563314,-3.60010298834566));
#17015=CARTESIAN_POINT('Ctrl Pts',(-3.01236018336962,-0.330292786539225,
-3.44095330852556));
#17016=CARTESIAN_POINT('Ctrl Pts',(-1.34974308024733,-2.71322701485407,
-3.28180362870545));
#17017=CARTESIAN_POINT('Ctrl Pts',(1.55374646135307,-2.60178382571544,-3.12265394888534));
#17018=CARTESIAN_POINT('Ctrl Pts',(3.02881515590367,-0.0984174171722393,
-2.96350426906523));
#17019=CARTESIAN_POINT('Ctrl Pts',(1.71937370994117,2.49542809128842,-2.80435458924512));
#17020=CARTESIAN_POINT('Ctrl Pts',(-1.17075626364219,2.7951272920322,-2.64520490942502));
#17021=CARTESIAN_POINT('Ctrl Pts',(-2.98456356430545,0.525155123988089,
-2.48605522960491));
#17022=CARTESIAN_POINT('Ctrl Pts',(-2.05454284140974,-2.22761342128229,
-2.3269055497848));
#17023=CARTESIAN_POINT('Ctrl Pts',(0.764300461397087,-2.93244766085287,
-2.16775586996469));
#17024=CARTESIAN_POINT('Ctrl Pts',(2.8804925346794,-0.941367734267301,-2.00860619014458));
#17025=CARTESIAN_POINT('Ctrl Pts',(2.34853230892687,1.91515179884014,-1.84945651032448));
#17026=CARTESIAN_POINT('Ctrl Pts',(-0.342524956916667,3.01099074165932,
-1.69030683050437));
#17027=CARTESIAN_POINT('Ctrl Pts',(-2.71868930179547,1.33871668279276,-1.53115715068426));
#17028=CARTESIAN_POINT('Ctrl Pts',(-2.59544711620706,-1.56431277364559,
-1.37200747086416));
#17029=CARTESIAN_POINT('Ctrl Pts',(-0.0861214973563786,-3.0291691303325,
-1.21285779104405));
#17030=CARTESIAN_POINT('Ctrl Pts',(2.5024062744662,-1.70926309947988,-1.05370811122394));
#17031=CARTESIAN_POINT('Ctrl Pts',(2.79032038025327,1.18217646775642,-0.894558431403832));
#17032=CARTESIAN_POINT('Ctrl Pts',(0.513081927707314,2.98652609954223,-0.735408751583725));
#17033=CARTESIAN_POINT('Ctrl Pts',(-2.23604427182097,2.04575701631777,-0.576259071763615));
#17034=CARTESIAN_POINT('Ctrl Pts',(-2.92912011817042,-0.776741122275152,
-0.41710939194351));
#17035=CARTESIAN_POINT('Ctrl Pts',(-0.930040753983942,-2.88326355857391,
-0.257959712123399));
#17036=CARTESIAN_POINT('Ctrl Pts',(1.92540990438357,-2.34273649504526,-0.0988100323032949));
#17037=CARTESIAN_POINT('Ctrl Pts',(3.00812651671163,0.358881109808823,0.0603396475168144));
#17038=CARTESIAN_POINT('Ctrl Pts',(1.88996995460182,1.92877590264587,0.166439434063553));
#17039=CARTESIAN_POINT('Ctrl Pts',(1.12236674703444,2.30288577939269,0.219489327336923));
#17040=CARTESIAN_POINT('Ctrl Pts',(0.439445221994093,2.33068358199189,-7.62825));
#17041=CARTESIAN_POINT('Ctrl Pts',(-0.337423613347535,2.47716047848903,
-7.57520010672663));
#17042=CARTESIAN_POINT('Ctrl Pts',(-2.03563801517394,1.92935211656188,-7.4691003201799));
#17043=CARTESIAN_POINT('Ctrl Pts',(-2.72493988491372,-0.675536495339759,
-7.30995064035978));
#17044=CARTESIAN_POINT('Ctrl Pts',(-0.903098151772226,-2.65539425532298,
-7.15080096053969));
#17045=CARTESIAN_POINT('Ctrl Pts',(1.74597935598366,-2.19600765141715,-6.99165128071957));
#17046=CARTESIAN_POINT('Ctrl Pts',(2.79147243493216,0.283269578050224,-6.83250160089946));
#17047=CARTESIAN_POINT('Ctrl Pts',(1.26983859810019,2.50159785776548,-6.67335192107936));
#17048=CARTESIAN_POINT('Ctrl Pts',(-1.4187825692111,2.42038344679719,-6.51420224125925));
#17049=CARTESIAN_POINT('Ctrl Pts',(-2.80328291203716,0.113870415496436,
-6.35505256143915));
#17050=CARTESIAN_POINT('Ctrl Pts',(-1.61049774213476,-2.29725302707627,
-6.19590288161903));
#17051=CARTESIAN_POINT('Ctrl Pts',(1.06282132621106,-2.59645975535387,-6.03675320179892));
#17052=CARTESIAN_POINT('Ctrl Pts',(2.75907820786381,-0.508617350322671,
-5.87760352197883));
#17053=CARTESIAN_POINT('Ctrl Pts',(1.91878831253368,2.04680647949509,-5.7184538421587));
#17054=CARTESIAN_POINT('Ctrl Pts',(-0.685511273604884,2.72052538198363,
-5.55930416233861));
#17055=CARTESIAN_POINT('Ctrl Pts',(-2.65959762385548,0.893154280769607,
-5.40015448251848));
#17056=CARTESIAN_POINT('Ctrl Pts',(-2.18860784384354,-1.75532751220894,
-5.2410048026984));
#17057=CARTESIAN_POINT('Ctrl Pts',(0.294454856588238,-2.79006777499793,
-5.08185512287827));
#17058=CARTESIAN_POINT('Ctrl Pts',(2.50681415110888,-1.25978745570213,-4.92270544305818));
#17059=CARTESIAN_POINT('Ctrl Pts',(2.41455925517875,1.42866531011816,-4.76355576323806));
#17060=CARTESIAN_POINT('Ctrl Pts',(0.102504271982408,2.80368940376361,-4.60440608341796));
#17061=CARTESIAN_POINT('Ctrl Pts',(-2.30378705302599,1.60117036795331,-4.44525640359785));
#17062=CARTESIAN_POINT('Ctrl Pts',(-2.59211535415612,-1.07336817656879,
-4.28610672377774));
#17063=CARTESIAN_POINT('Ctrl Pts',(-0.497409040646124,-2.76111672375383,
-4.12695704395763));
#17064=CARTESIAN_POINT('Ctrl Pts',(2.05458518082845,-1.91046094844367,-3.96780736413752));
#17065=CARTESIAN_POINT('Ctrl Pts',(2.717717602526,0.69655748161016,-3.80865768431742));
#17066=CARTESIAN_POINT('Ctrl Pts',(0.882344250202438,2.66320294535576,-3.64950800449731));
#17067=CARTESIAN_POINT('Ctrl Pts',(-1.76420323128872,2.18146011904347,-3.4903583246772));
#17068=CARTESIAN_POINT('Ctrl Pts',(-2.7888485843108,-0.305785667740972,
-3.33120864485709));
#17069=CARTESIAN_POINT('Ctrl Pts',(-1.24959461996354,-2.51191054810233,
-3.17205896503699));
#17070=CARTESIAN_POINT('Ctrl Pts',(1.43846132446067,-2.40873623914147,-3.01290928521687));
#17071=CARTESIAN_POINT('Ctrl Pts',(2.80408262807151,-0.0911150253769769,
-2.85375960539677));
#17072=CARTESIAN_POINT('Ctrl Pts',(1.59179933506719,2.3102719050862,-2.69460992557666));
#17073=CARTESIAN_POINT('Ctrl Pts',(-1.08388829677707,2.58773397497002,-2.53546024575656));
#17074=CARTESIAN_POINT('Ctrl Pts',(-2.76311442338486,0.486189577250177,
-2.37631056593645));
#17075=CARTESIAN_POINT('Ctrl Pts',(-1.90209953189,-2.0623285922554,-2.21716088611634));
#17076=CARTESIAN_POINT('Ctrl Pts',(0.707590769365126,-2.71486542435539,
-2.05801120629623));
#17077=CARTESIAN_POINT('Ctrl Pts',(2.66676527322589,-0.871519975440165,
-1.89886152647612));
#17078=CARTESIAN_POINT('Ctrl Pts',(2.17427552027739,1.77305104894897,-1.73971184665602));
#17079=CARTESIAN_POINT('Ctrl Pts',(-0.31711023351784,2.787580752663,-1.58056216683591));
#17080=CARTESIAN_POINT('Ctrl Pts',(-2.51696754337392,1.23938636097081,-1.4214124870158));
#17081=CARTESIAN_POINT('Ctrl Pts',(-2.40286970185313,-1.44824363576629,
-1.26226280719569));
#17082=CARTESIAN_POINT('Ctrl Pts',(-0.0797314402530648,-2.80441033824713,
-1.10311312737558));
#17083=CARTESIAN_POINT('Ctrl Pts',(2.31673231987452,-1.58243891335296,-0.94396344755548));
#17084=CARTESIAN_POINT('Ctrl Pts',(2.58328372722621,1.0944611426978,-0.784813767735368));
#17085=CARTESIAN_POINT('Ctrl Pts',(0.47501218998366,2.76493134210758,-0.625664087915265));
#17086=CARTESIAN_POINT('Ctrl Pts',(-2.07013388915155,1.89396559890118,-0.466514408095153));
#17087=CARTESIAN_POINT('Ctrl Pts',(-2.71178477923519,-0.719108356029971,
-0.307364728275049));
#17088=CARTESIAN_POINT('Ctrl Pts',(-0.861033436313082,-2.66933069223121,
-0.148215048454937));
#17089=CARTESIAN_POINT('Ctrl Pts',(1.78254802188085,-2.16890974515266,0.0109346313651662));
#17090=CARTESIAN_POINT('Ctrl Pts',(2.78492904795165,0.332252789872783,0.170084311185276));
#17091=CARTESIAN_POINT('Ctrl Pts',(1.74973765135393,1.78566426924742,0.276184097732015));
#17092=CARTESIAN_POINT('Ctrl Pts',(1.03908919352505,2.13201587949045,0.329233991005384));
#17093=CARTESIAN_POINT('',(1.28892185405323,2.64462557919718,0.));
#17094=CARTESIAN_POINT('Ctrl Pts',(1.28892185405323,2.64462557919718,0.));
#17095=CARTESIAN_POINT('Ctrl Pts',(2.17043456109762,2.21499916944277,-0.0530498932733694));
#17096=CARTESIAN_POINT('Ctrl Pts',(2.8124780076646,1.31356845956184,-0.106099786546739));
#17097=CARTESIAN_POINT('Ctrl Pts',(2.92626843347433,0.345765147202809,-0.159149679820108));
#17098=CARTESIAN_POINT('Ctrl Pts',(3.04005885928406,-0.622038165156221,
-0.212199573093478));
#17099=CARTESIAN_POINT('Ctrl Pts',(2.62559626433654,-1.65621407999334,-0.265249466366847));
#17100=CARTESIAN_POINT('Ctrl Pts',(1.871833457077,-2.27675858681671,-0.318299359640216));
#17101=CARTESIAN_POINT('Ctrl Pts',(1.11807064981746,-2.89730309364007,-0.371349252913585));
#17102=CARTESIAN_POINT('Ctrl Pts',(0.0250076302459046,-3.10421619244968,
-0.424399146186955));
#17103=CARTESIAN_POINT('Ctrl Pts',(-0.904146447325742,-2.80448563577219,
-0.477449039460324));
#17104=CARTESIAN_POINT('Ctrl Pts',(-1.8333005248974,-2.5047550790947,-0.530498932733693));
#17105=CARTESIAN_POINT('Ctrl Pts',(-2.59854566046914,-1.69838086693011,
-0.583548826007063));
#17106=CARTESIAN_POINT('Ctrl Pts',(-2.84851393510817,-0.754969343195062,
-0.636598719280432));
#17107=CARTESIAN_POINT('Ctrl Pts',(-2.91326419433548,-0.510593768702306,
-0.650340440490422));
#17108=CARTESIAN_POINT('Ctrl Pts',(-2.94344011517888,-0.25702318713533,
-0.664082161700412));
#17109=CARTESIAN_POINT('Ctrl Pts',(-2.94115781190101,-0.00289931852541142,
-0.677823882910403));
#17110=CARTESIAN_POINT('Ctrl Pts',(1.38002164928817,-1.93382042716839,-7.7715611723761E-16));
#17111=CARTESIAN_POINT('Ctrl Pts',(1.42812747073086,-1.90764311681531,-7.5694502902296E-16));
#17112=CARTESIAN_POINT('Ctrl Pts',(1.47517679419513,-1.87973274797267,-1.70831917836036E-15));
#17113=CARTESIAN_POINT('Ctrl Pts',(1.52106467934594,-1.85010961136059,-1.94289029309402E-15));
#17114=CARTESIAN_POINT('Ctrl Pts',(1.58950048722442,-1.80593055888783,-2.29363597887594E-15));
#17115=CARTESIAN_POINT('Ctrl Pts',(1.65535434494963,-1.7579446136614,-3.02182188661513E-15));
#17116=CARTESIAN_POINT('Ctrl Pts',(1.71854070901811,-1.70651204529061,-3.60822483003176E-15));
#17117=CARTESIAN_POINT('Ctrl Pts',(1.7555130642401,-1.67641721049804,-3.95134787955118E-15));
#17118=CARTESIAN_POINT('Ctrl Pts',(1.79157183927568,-1.64514134213701,-1.07060037084947E-15));
#17119=CARTESIAN_POINT('Ctrl Pts',(1.82669682228498,-1.61274915084688,-1.16573417585641E-15));
#17120=CARTESIAN_POINT('Ctrl Pts',(1.841722159954,-1.59889281355429,-1.20642935693563E-15));
#17121=CARTESIAN_POINT('Ctrl Pts',(1.85657659510814,-1.58483214201628,-3.58134186129285E-15));
#17122=CARTESIAN_POINT('Ctrl Pts',(1.87125839132482,-1.57057192863285,-3.77475828372553E-15));
#17123=CARTESIAN_POINT('Ctrl Pts',(1.88495537365188,-1.5572682505399,-3.95520087267901E-15));
#17124=CARTESIAN_POINT('Ctrl Pts',(1.89850308492679,-1.54378970611349,-1.28299784462317E-15));
#17125=CARTESIAN_POINT('Ctrl Pts',(1.91188526750315,-1.53015568567424,-1.33226762955019E-15));
#17126=CARTESIAN_POINT('Ctrl Pts',(1.97177620973344,-1.46913766220646,-1.5527708117424E-15));
#17127=CARTESIAN_POINT('Ctrl Pts',(2.02842345123512,-1.40494307633604,-3.57723878703623E-15));
#17128=CARTESIAN_POINT('Ctrl Pts',(2.0817308935379,-1.33796367996907,-3.44169137633799E-15));
#17129=CARTESIAN_POINT('Ctrl Pts',(2.127945639128,-1.2798960700977,-3.32417890846838E-15));
#17130=CARTESIAN_POINT('Ctrl Pts',(2.17165011443041,-1.21973426244966,-1.81697204400015E-15));
#17131=CARTESIAN_POINT('Ctrl Pts',(2.21276616256005,-1.15770575782311,-1.83186799063151E-15));
#17132=CARTESIAN_POINT('Ctrl Pts',(2.2325537470201,-1.12785380633305,-1.83903684112879E-15));
#17133=CARTESIAN_POINT('Ctrl Pts',(2.25174157820912,-1.09756915706639,-2.28535431450448E-15));
#17134=CARTESIAN_POINT('Ctrl Pts',(2.27031947398645,-1.06687542421666,-2.58126853225349E-15));
#17135=CARTESIAN_POINT('Ctrl Pts',(2.28192871071775,-1.04769505981529,-2.76618388796334E-15));
#17136=CARTESIAN_POINT('Ctrl Pts',(2.29330289136903,-1.02834915196317,6.32263275798518E-17));
#17137=CARTESIAN_POINT('Ctrl Pts',(2.30442183390172,-1.00887472850267,5.55111512312578E-17));
#17138=CARTESIAN_POINT('Ctrl Pts',(2.34839407475996,-0.931858947868614,
2.49998331210308E-17));
#17139=CARTESIAN_POINT('Ctrl Pts',(2.38842162089745,-0.8527674310775,-3.06551327022485E-15));
#17140=CARTESIAN_POINT('Ctrl Pts',(2.42440442503016,-0.771996655564967,
-2.72004641033163E-15));
#17141=CARTESIAN_POINT('Ctrl Pts',(2.46243949056497,-0.686619158897789,
-2.35487601928374E-15));
#17142=CARTESIAN_POINT('Ctrl Pts',(2.49595626081657,-0.599364864549967,
6.80623617719379E-16));
#17143=CARTESIAN_POINT('Ctrl Pts',(2.52479802771902,-0.510654497756694,
1.27675647831893E-15));
#17144=CARTESIAN_POINT('Ctrl Pts',(2.55242599313135,-0.425677493616475,
1.84780117573675E-15));
#17145=CARTESIAN_POINT('Ctrl Pts',(2.57576446764424,-0.33936327234262,2.22743437905015E-16));
#17146=CARTESIAN_POINT('Ctrl Pts',(2.59463283383731,-0.252052712602013,
2.77555756156289E-16));
#17147=CARTESIAN_POINT('Ctrl Pts',(2.60106539892371,-0.222286973877501,
2.96242260386698E-16));
#17148=CARTESIAN_POINT('Ctrl Pts',(2.60697802607669,-0.192405253045208,
-1.3763582714056E-15));
#17149=CARTESIAN_POINT('Ctrl Pts',(2.61236225462784,-0.162420585421049,
-1.4432899320127E-15));
#17150=CARTESIAN_POINT('Ctrl Pts',(2.61541762236764,-0.145405299892759,
-1.48127138741476E-15));
#17151=CARTESIAN_POINT('Ctrl Pts',(2.61830282357874,-0.128356860267427,
-2.88095861055776E-15));
#17152=CARTESIAN_POINT('Ctrl Pts',(2.62101620860007,-0.111277626913365,
-2.99760216648792E-15));
#17153=CARTESIAN_POINT('Ctrl Pts',(2.62313739988994,-0.0979259201914906,
-3.08878837593249E-15));
#17154=CARTESIAN_POINT('Ctrl Pts',(2.62515315328059,-0.0845577480124575,
-1.4025265292375E-15));
#17155=CARTESIAN_POINT('Ctrl Pts',(2.62706136230965,-0.0711852941876254,
-1.36002320516582E-15));
#17156=CARTESIAN_POINT('Ctrl Pts',(2.64014127982351,0.0204768823995774,
-1.06868197134027E-15));
#17157=CARTESIAN_POINT('Ctrl Pts',(2.64819506516295,0.112482484208663,-2.30351243816908E-15));
#17158=CARTESIAN_POINT('Ctrl Pts',(2.65108741954648,0.204436910520549,-2.13717932240343E-15));
#17159=CARTESIAN_POINT('Ctrl Pts',(2.6522300189544,0.240762705747386,-2.07147087371765E-15));
#17160=CARTESIAN_POINT('Ctrl Pts',(2.6525666724142,0.277080849976937,1.38410269878359E-15));
#17161=CARTESIAN_POINT('Ctrl Pts',(2.65208709596217,0.313368136238073,1.36002320516582E-15));
#17162=CARTESIAN_POINT('Ctrl Pts',(2.65091611137812,0.401971012023442,1.30322121910574E-15));
#17163=CARTESIAN_POINT('Ctrl Pts',(2.64488261707637,0.490389342189787,3.16280801020804E-17));
#17164=CARTESIAN_POINT('Ctrl Pts',(2.6342319072788,0.578361332654982,-1.38777878078145E-16));
#17165=CARTESIAN_POINT('Ctrl Pts',(2.62336505681307,0.668118586746737,-3.12641977392605E-16));
#17166=CARTESIAN_POINT('Ctrl Pts',(2.60769159491865,0.757411929633459,-1.18972610440493E-15));
#17167=CARTESIAN_POINT('Ctrl Pts',(2.58741809056973,0.845967129974637,-1.22124532708767E-15));
#17168=CARTESIAN_POINT('Ctrl Pts',(2.58188375720388,0.870141243711141,-1.22984955666519E-15));
#17169=CARTESIAN_POINT('Ctrl Pts',(2.57600632881146,0.894260336658512,-2.52103891604412E-15));
#17170=CARTESIAN_POINT('Ctrl Pts',(2.56978934466171,0.918318763783367,-2.65065747129256E-15));
#17171=CARTESIAN_POINT('Ctrl Pts',(2.56617655991,0.932299484430771,-2.72598079988109E-15));
#17172=CARTESIAN_POINT('Ctrl Pts',(2.56245121029721,0.946251475332682,-1.21864460931396E-15));
#17173=CARTESIAN_POINT('Ctrl Pts',(2.55861555514304,0.960169583265971,-1.17961196366423E-15));
#17174=CARTESIAN_POINT('Ctrl Pts',(2.53400743126124,1.0494629400605,-9.29193158799269E-16));
#17175=CARTESIAN_POINT('Ctrl Pts',(2.5048497143222,1.13741458886572,-5.45198539607864E-16));
#17176=CARTESIAN_POINT('Ctrl Pts',(2.47143088982083,1.22374100902459,-3.33066907387547E-16));
#17177=CARTESIAN_POINT('Ctrl Pts',(2.43737301009748,1.31171821584098,-1.16878764223515E-16));
#17178=CARTESIAN_POINT('Ctrl Pts',(2.39888933062496,1.39800823053115,9.879708656971E-16));
#17179=CARTESIAN_POINT('Ctrl Pts',(2.35622978660644,1.48231381194112,1.29063426612674E-15));
#17180=CARTESIAN_POINT('Ctrl Pts',(2.31321870904863,1.56731410868612,1.59579174704448E-15));
#17181=CARTESIAN_POINT('Ctrl Pts',(2.26596236943433,1.65029800809477,-2.42731618613007E-15));
#17182=CARTESIAN_POINT('Ctrl Pts',(2.21466476470311,1.73095108378988,-2.63677968348475E-15));
#17183=CARTESIAN_POINT('Ctrl Pts',(2.18386460320696,1.77937688787153,-2.76254597569037E-15));
#17184=CARTESIAN_POINT('Ctrl Pts',(2.15160656205411,1.82696217117237,-2.40998514952242E-15));
#17185=CARTESIAN_POINT('Ctrl Pts',(2.11792656714594,1.87363515402618,-2.49106291150269E-15));
#17186=CARTESIAN_POINT('Ctrl Pts',(2.10877443900116,1.88631796829447,-2.51309480519384E-15));
#17187=CARTESIAN_POINT('Ctrl Pts',(2.09951639417844,1.89893445563434,-2.77486678097692E-15));
#17188=CARTESIAN_POINT('Ctrl Pts',(2.09016420919922,1.91146858929654,-2.69922972861991E-15));
#17189=CARTESIAN_POINT('Ctrl Pts',(2.03135556865992,1.99028603812276,-2.22360694812491E-15));
#17190=CARTESIAN_POINT('Ctrl Pts',(1.96873479008562,2.06598007149761,-4.57292501631552E-16));
#17191=CARTESIAN_POINT('Ctrl Pts',(1.90257280213557,2.13824089870506,-6.38378239159465E-16));
#17192=CARTESIAN_POINT('Ctrl Pts',(1.83625579712803,2.2106710325061,-8.19888259255879E-16));
#17193=CARTESIAN_POINT('Ctrl Pts',(1.76638056903207,2.27965275545374,1.58499855722304E-15));
#17194=CARTESIAN_POINT('Ctrl Pts',(1.69316997818223,2.3448583260052,1.31492039479042E-15));
#17195=CARTESIAN_POINT('Ctrl Pts',(1.62138713583198,2.4087922614771,1.05010928029049E-15));
#17196=CARTESIAN_POINT('Ctrl Pts',(1.54639722394925,2.46909666244371,4.27974250822394E-16));
#17197=CARTESIAN_POINT('Ctrl Pts',(1.46836948021005,2.52543520618547,1.07552855510562E-15));
#17198=CARTESIAN_POINT('Ctrl Pts',(1.4102223701464,2.56741929218862,1.55809295590647E-15));
#17199=CARTESIAN_POINT('Ctrl Pts',(1.35038736882638,2.60720050088858,6.55137100424993E-17));
#17200=CARTESIAN_POINT('Ctrl Pts',(1.28892185405323,2.64462557919718,0.));
#17201=CARTESIAN_POINT('Ctrl Pts',(0.439445221994093,2.33068358199189,-7.62825));
#17202=CARTESIAN_POINT('Ctrl Pts',(-0.337423613347535,2.47716047848903,
-7.57520010672663));
#17203=CARTESIAN_POINT('Ctrl Pts',(-1.82948700838562,1.99585210927004,-7.48198007069497));
#17204=CARTESIAN_POINT('Ctrl Pts',(-2.3653507640067,0.596861175155798,-7.38876003466331));
#17205=CARTESIAN_POINT('Ctrl Pts',(-2.37144645257593,-0.00213225654898062,
-7.34858989190502));
#17206=CARTESIAN_POINT('Origin',(0.,0.,-8.));
#17207=CARTESIAN_POINT('',(-1.28892185405322,2.64462557919718,0.));
#17208=CARTESIAN_POINT('Ctrl Pts',(-2.94163492837973,-0.00273205723265913,
-0.822176117089598));
#17209=CARTESIAN_POINT('Ctrl Pts',(-2.94382357462719,-0.242779219769019,
-0.809190456057937));
#17210=CARTESIAN_POINT('Ctrl Pts',(-2.91690973953269,-0.48233937851609,
-0.796204795026276));
#17211=CARTESIAN_POINT('Ctrl Pts',(-2.85900606151163,-0.714154570807424,
-0.783219133994616));
#17212=CARTESIAN_POINT('Ctrl Pts',(-2.62279267049859,-1.65982597771804,
-0.730245175661282));
#17213=CARTESIAN_POINT('Ctrl Pts',(-1.87085675264489,-2.47660826181784,
-0.677271217327949));
#17214=CARTESIAN_POINT('Ctrl Pts',(-0.947905463978179,-2.79019041180322,
-0.624297258994615));
#17215=CARTESIAN_POINT('Ctrl Pts',(-0.0249541753114783,-3.1037725617886,
-0.571323300661282));
#17216=CARTESIAN_POINT('Ctrl Pts',(1.06901248416821,-2.91415457765955,-0.518349342327949));
#17217=CARTESIAN_POINT('Ctrl Pts',(1.832390730231,-2.30797131654626,-0.465375383994615));
#17218=CARTESIAN_POINT('Ctrl Pts',(2.59576897629379,-1.70178805543296,-0.412401425661282));
#17219=CARTESIAN_POINT('Ctrl Pts',(3.02855880893968,-0.679039517335424,
-0.359427467327948));
#17220=CARTESIAN_POINT('Ctrl Pts',(2.93245036408289,0.290806479998895,-0.306453508994615));
#17221=CARTESIAN_POINT('Ctrl Pts',(2.83634191922609,1.26065247733321,-0.253479550661282));
#17222=CARTESIAN_POINT('Ctrl Pts',(2.21133519686661,2.17759593390431,-0.200505592327948));
#17223=CARTESIAN_POINT('Ctrl Pts',(1.34376500468284,2.62235303498606,-0.147531633994614));
#17224=CARTESIAN_POINT('Ctrl Pts',(0.538375261717025,3.03523352644325,-0.0983544226630757));
#17225=CARTESIAN_POINT('Ctrl Pts',(-0.476053973012966,3.04118713875837,
-0.0491772113315374));
#17226=CARTESIAN_POINT('Ctrl Pts',(-1.29202279186848,2.64852742499071,1.17961196366423E-15));
#17227=CARTESIAN_POINT('Origin',(0.,0.,0.));
#17228=CARTESIAN_POINT('Origin',(1.15470053837925,2.,28.));
#17229=CARTESIAN_POINT('',(1.15470053837925,2.,28.));
#17230=CARTESIAN_POINT('',(2.3094010767585,0.,28.));
#17231=CARTESIAN_POINT('',(1.44337567297406,1.5,28.));
#17232=CARTESIAN_POINT('',(1.15470053837925,2.,25.));
#17233=CARTESIAN_POINT('',(1.15470053837925,2.,28.));
#17234=CARTESIAN_POINT('',(2.3094010767585,0.,25.));
#17235=CARTESIAN_POINT('',(2.3094010767585,0.,25.));
#17236=CARTESIAN_POINT('',(2.3094010767585,0.,28.));
#17237=CARTESIAN_POINT('Origin',(-1.15470053837925,2.,28.));
#17238=CARTESIAN_POINT('',(-1.15470053837925,2.,28.));
#17239=CARTESIAN_POINT('',(-0.577350269189626,2.,28.));
#17240=CARTESIAN_POINT('',(-1.15470053837925,2.,25.));
#17241=CARTESIAN_POINT('',(-1.15470053837925,2.,28.));
#17242=CARTESIAN_POINT('',(1.15470053837925,2.,25.));
#17243=CARTESIAN_POINT('Origin',(-2.3094010767585,2.77555756156289E-16,
28.));
#17244=CARTESIAN_POINT('',(-2.3094010767585,2.82820063659975E-16,28.));
#17245=CARTESIAN_POINT('',(-2.02072594216369,0.5,28.));
#17246=CARTESIAN_POINT('',(-2.3094010767585,2.77555756156289E-16,25.));
#17247=CARTESIAN_POINT('',(-2.3094010767585,2.82820063659975E-16,28.));
#17248=CARTESIAN_POINT('',(-1.15470053837925,2.,25.));
#17249=CARTESIAN_POINT('Origin',(-1.15470053837925,-2.,28.));
#17250=CARTESIAN_POINT('',(-1.15470053837925,-2.,28.));
#17251=CARTESIAN_POINT('',(-1.44337567297407,-1.5,28.));
#17252=CARTESIAN_POINT('',(-1.15470053837925,-2.,25.));
#17253=CARTESIAN_POINT('',(-1.15470053837925,-2.,28.));
#17254=CARTESIAN_POINT('',(-2.3094010767585,2.82820063659975E-16,25.));
#17255=CARTESIAN_POINT('Origin',(1.15470053837925,-2.,28.));
#17256=CARTESIAN_POINT('',(1.15470053837925,-2.,28.));
#17257=CARTESIAN_POINT('',(0.577350269189626,-2.,28.));
#17258=CARTESIAN_POINT('',(1.15470053837925,-2.,25.));
#17259=CARTESIAN_POINT('',(1.15470053837925,-2.,28.));
#17260=CARTESIAN_POINT('',(-1.15470053837925,-2.,25.));
#17261=CARTESIAN_POINT('Origin',(2.3094010767585,0.,28.));
#17262=CARTESIAN_POINT('',(2.02072594216369,-0.5,28.));
#17263=CARTESIAN_POINT('',(1.15470053837925,-2.,25.));
#17264=CARTESIAN_POINT('Origin',(0.,0.,25.));
#17265=CARTESIAN_POINT('Ctrl Pts',(2.34668236863854,0.343918483395443,-7.62825));
#17266=CARTESIAN_POINT('Ctrl Pts',(2.23221075339669,1.12500043789087,-7.57527604166667));
#17267=CARTESIAN_POINT('Ctrl Pts',(1.16389372259185,2.55030135594479,-7.469328125));
#17268=CARTESIAN_POINT('Ctrl Pts',(-1.5190222941925,2.35934508271871,-7.31040625));
#17269=CARTESIAN_POINT('Ctrl Pts',(-2.80340787029919,0.000687648512017017,
-7.15148437500001));
#17270=CARTESIAN_POINT('Ctrl Pts',(-1.52008573002868,-2.35640251272322,
-6.99256249999999));
#17271=CARTESIAN_POINT('Ctrl Pts',(1.15851212495977,-2.55397203032575,-6.833640625));
#17272=CARTESIAN_POINT('Ctrl Pts',(2.77407199314419,-0.40912796830676,-6.67471874999999));
#17273=CARTESIAN_POINT('Ctrl Pts',(1.8463937974617,2.11054799657883,-6.515796875));
#17274=CARTESIAN_POINT('Ctrl Pts',(-0.774509592452447,2.6951571659338,-6.356875));
#17275=CARTESIAN_POINT('Ctrl Pts',(-2.68513189196673,0.808405636158886,
-6.197953125));
#17276=CARTESIAN_POINT('Ctrl Pts',(-2.13372739995655,-1.81955463387985,
-6.03903125));
#17277=CARTESIAN_POINT('Ctrl Pts',(0.374189682251391,-2.77913011091259,
-5.88010937499999));
#17278=CARTESIAN_POINT('Ctrl Pts',(2.53898480026785,-1.19042008723587,-5.7211875));
#17279=CARTESIAN_POINT('Ctrl Pts',(2.37571150505774,1.48981793161623,-5.562265625));
#17280=CARTESIAN_POINT('Ctrl Pts',(0.0340680162793398,2.80399746681091,
-5.40334375));
#17281=CARTESIAN_POINT('Ctrl Pts',(-2.33881132397979,1.54710018774848,-5.244421875));
#17282=CARTESIAN_POINT('Ctrl Pts',(-2.56716079869307,-1.12838190825516,
-5.0855));
#17283=CARTESIAN_POINT('Ctrl Pts',(-0.441597707549828,-2.76921495982712,
-4.926578125));
#17284=CARTESIAN_POINT('Ctrl Pts',(2.0888801521554,-1.870865869044,-4.76765625));
#17285=CARTESIAN_POINT('Ctrl Pts',(2.70399705609256,0.742939933921091,-4.608734375));
#17286=CARTESIAN_POINT('Ctrl Pts',(0.839732362462355,2.67552038173531,-4.4498125));
#17287=CARTESIAN_POINT('Ctrl Pts',(-1.79450978671873,2.15483045727933,-4.290890625));
#17288=CARTESIAN_POINT('Ctrl Pts',(-2.78330845646984,-0.341692515414928,
-4.13196875));
#17289=CARTESIAN_POINT('Ctrl Pts',(-1.22000243857572,-2.52490668674665,
-3.973046875));
#17290=CARTESIAN_POINT('Ctrl Pts',(1.46196288604333,-2.39295303517309,-3.814125));
#17291=CARTESIAN_POINT('Ctrl Pts',(2.80340761681022,-0.0668241043267523,
-3.655203125));
#17292=CARTESIAN_POINT('Ctrl Pts',(1.57431810519612,2.32057799752537,-3.49628125));
#17293=CARTESIAN_POINT('Ctrl Pts',(-1.09831409983361,2.58016778763604,-3.337359375));
#17294=CARTESIAN_POINT('Ctrl Pts',(-2.76386693296932,0.47391911808494,-3.1784375));
#17295=CARTESIAN_POINT('Ctrl Pts',(-1.89514163556503,-2.06688122685359,
-3.019515625));
#17296=CARTESIAN_POINT('Ctrl Pts',(0.71129970966804,-2.71249186414424,-2.86059375));
#17297=CARTESIAN_POINT('Ctrl Pts',(2.66552760696098,-0.870932032693957,
-2.701671875));
#17298=CARTESIAN_POINT('Ctrl Pts',(2.17564778740008,1.76921366782114,-2.54275));
#17299=CARTESIAN_POINT('Ctrl Pts',(-0.309153032213342,2.78710993733308,
-2.383828125));
#17300=CARTESIAN_POINT('Ctrl Pts',(-2.51048180952901,1.24941726722468,-2.22490625));
#17301=CARTESIAN_POINT('Ctrl Pts',(-2.40986887600225,-1.43390886220311,
-2.065984375));
#17302=CARTESIAN_POINT('Ctrl Pts',(-0.0995709890729291,-2.80243276783242,
-1.9070625));
#17303=CARTESIAN_POINT('Ctrl Pts',(2.30202865838936,-1.60132637136797,-1.748140625));
#17304=CARTESIAN_POINT('Ctrl Pts',(2.59282079624265,1.06810673697464,-1.58921875));
#17305=CARTESIAN_POINT('Ctrl Pts',(0.506179573027947,2.75812167782342,-1.430296875));
#17306=CARTESIAN_POINT('Ctrl Pts',(-2.04460746115808,1.91919712058503,-1.271375));
#17307=CARTESIAN_POINT('Ctrl Pts',(-2.72060249130678,-0.679635921257337,
-1.112453125));
#17308=CARTESIAN_POINT('Ctrl Pts',(-0.902039595484687,-2.65503026080224,
-0.953531249999998));
#17309=CARTESIAN_POINT('Ctrl Pts',(1.74372732289156,-2.19643768378856,-0.794609375000001));
#17310=CARTESIAN_POINT('Ctrl Pts',(2.79043291661474,0.277087651255129,-0.635687499999998));
#17311=CARTESIAN_POINT('Ctrl Pts',(1.2788492724039,2.49472256946297,-0.476765624999999));
#17312=CARTESIAN_POINT('Ctrl Pts',(-1.4060176679778,2.42838470324144,-0.317843749999998));
#17313=CARTESIAN_POINT('Ctrl Pts',(-2.80039548414902,0.128338365192599,
-0.158921874999999));
#17314=CARTESIAN_POINT('Ctrl Pts',(-2.01976953076572,-1.47272600147648,
-0.0529739583333322));
#17315=CARTESIAN_POINT('Ctrl Pts',(-1.37702479013101,-1.93106208855766,
1.11022302462516E-15));
#17316=CARTESIAN_POINT('Ctrl Pts',(2.53475666268529,0.371481747533205,-7.51850533633154));
#17317=CARTESIAN_POINT('Ctrl Pts',(2.41111074737083,1.2151633274179,-7.4655313779982));
#17318=CARTESIAN_POINT('Ctrl Pts',(1.25717370506724,2.75469464475791,-7.35958346133153));
#17319=CARTESIAN_POINT('Ctrl Pts',(-1.64076397062878,2.54843422693997,-7.20066158633155));
#17320=CARTESIAN_POINT('Ctrl Pts',(-3.02808631983197,0.000742759936635549,
-7.04173971133153));
#17321=CARTESIAN_POINT('Ctrl Pts',(-1.6419126352743,-2.54525582537989,-6.88281783633154));
#17322=CARTESIAN_POINT('Ctrl Pts',(1.25136080058723,-2.75865950445431,-6.72389596133153));
#17323=CARTESIAN_POINT('Ctrl Pts',(2.99639932585779,-0.441917430929573,
-6.56497408633154));
#17324=CARTESIAN_POINT('Ctrl Pts',(1.99437258429316,2.27969735816824,-6.40605221133153));
#17325=CARTESIAN_POINT('Ctrl Pts',(-0.836582477466464,2.91115988880001,
-6.24713033633154));
#17326=CARTESIAN_POINT('Ctrl Pts',(-2.90033114166196,0.873195111443611,
-6.08820846133153));
#17327=CARTESIAN_POINT('Ctrl Pts',(-2.30473446925493,-1.96538240240098,
-5.92928658633154));
#17328=CARTESIAN_POINT('Ctrl Pts',(0.404179024341101,-3.00186282525825,
-5.77036471133153));
#17329=CARTESIAN_POINT('Ctrl Pts',(2.74247112644792,-1.28582601882594,-5.61144283633154));
#17330=CARTESIAN_POINT('Ctrl Pts',(2.56611233226117,1.60921903143761,-5.45252096133153));
#17331=CARTESIAN_POINT('Ctrl Pts',(0.0367983892505396,3.02872316941433,
-5.29359908633154));
#17332=CARTESIAN_POINT('Ctrl Pts',(-2.52625479504538,1.67109216021095,-5.13467721133154));
#17333=CARTESIAN_POINT('Ctrl Pts',(-2.77290528349047,-1.21881580491128,
-4.97575533633154));
#17334=CARTESIAN_POINT('Ctrl Pts',(-0.476989449615156,-2.99115302677367,
-4.81683346133153));
#17335=CARTESIAN_POINT('Ctrl Pts',(2.25629294956471,-2.02080596416678,-4.65791158633154));
#17336=CARTESIAN_POINT('Ctrl Pts',(2.9207082498295,0.802482676244758,-4.49898971133153));
#17337=CARTESIAN_POINT('Ctrl Pts',(0.907032510692453,2.88994931925466,-4.34006783633155));
#17338=CARTESIAN_POINT('Ctrl Pts',(-1.93833034198753,2.32752882603146,-4.18114596133153));
#17339=CARTESIAN_POINT('Ctrl Pts',(-3.00637604331527,-0.369077379884247,
-4.02222408633155));
#17340=CARTESIAN_POINT('Ctrl Pts',(-1.31777924059923,-2.72726472590441,
-3.86330221133153));
#17341=CARTESIAN_POINT('Ctrl Pts',(1.57913154993654,-2.58473568066095,-3.70438033633154));
#17342=CARTESIAN_POINT('Ctrl Pts',(3.02808604602719,-0.0721797060965247,
-3.54545846133154));
#17343=CARTESIAN_POINT('Ctrl Pts',(1.7004914511064,2.50656016302747,-3.38653658633154));
#17344=CARTESIAN_POINT('Ctrl Pts',(-1.18633821921523,2.78695471443404,-3.22761471133154));
#17345=CARTESIAN_POINT('Ctrl Pts',(-2.98537638358957,0.511901251824159,
-3.06869283633154));
#17346=CARTESIAN_POINT('Ctrl Pts',(-2.04702730615721,-2.23253092568543,
-2.90977096133154));
#17347=CARTESIAN_POINT('Ctrl Pts',(0.768306653828565,-2.92988387222945,
-2.75084908633154));
#17348=CARTESIAN_POINT('Ctrl Pts',(2.87915567594935,-0.940732670991103,
-2.59192721133154));
#17349=CARTESIAN_POINT('Ctrl Pts',(2.35001455606807,1.91100687172472,-2.43300533633154));
#17350=CARTESIAN_POINT('Ctrl Pts',(-0.333930027627364,3.01048219294801,
-2.27408346133154));
#17351=CARTESIAN_POINT('Ctrl Pts',(-2.71168377037141,1.34955151361587,-2.11516158633154));
#17352=CARTESIAN_POINT('Ctrl Pts',(-2.60300723748502,-1.54882914310277,
-1.95623971133154));
#17353=CARTESIAN_POINT('Ctrl Pts',(-0.10755108204491,-3.02703306801251,
-1.79731783633154));
#17354=CARTESIAN_POINT('Ctrl Pts',(2.48652419156761,-1.72966428827498,-1.63839596133154));
#17355=CARTESIAN_POINT('Ctrl Pts',(2.80062179537232,1.15370989452494,-1.47947408633154));
#17356=CARTESIAN_POINT('Ctrl Pts',(0.546747213169786,2.97917067635177,-1.32055221133154));
#17357=CARTESIAN_POINT('Ctrl Pts',(-2.20847203439519,2.07301071223869,-1.16163033633154));
#17358=CARTESIAN_POINT('Ctrl Pts',(-2.93864452365529,-0.734105178710968,
-1.00270846133154));
#17359=CARTESIAN_POINT('Ctrl Pts',(-0.974333341920184,-2.86781702250738,
-0.843786586331539));
#17360=CARTESIAN_POINT('Ctrl Pts',(1.88347792981034,-2.37247065370254,-0.684864711331538));
#17361=CARTESIAN_POINT('Ctrl Pts',(3.01407149160502,0.299294774424126,-0.525942836331538));
#17362=CARTESIAN_POINT('Ctrl Pts',(1.38134233977164,2.69466150980045,-0.367020961331536));
#17363=CARTESIAN_POINT('Ctrl Pts',(-1.51870261582422,2.62300701124516,-0.208099086331538));
#17364=CARTESIAN_POINT('Ctrl Pts',(-3.02483250671829,0.138624012605004,
-0.0491772113315371));
#17365=CARTESIAN_POINT('Ctrl Pts',(-2.18164347404518,-1.5907572726675,0.0567707053351293));
#17366=CARTESIAN_POINT('Ctrl Pts',(-1.48738611075533,-2.08582659521589,
0.109744663668463));
#17367=CARTESIAN_POINT('Ctrl Pts',(2.72283095673204,0.399045011670968,-7.40876067266308));
#17368=CARTESIAN_POINT('Ctrl Pts',(2.59001074134497,1.30532621694494,-7.35578671432974));
#17369=CARTESIAN_POINT('Ctrl Pts',(1.35045368754263,2.95908793357102,-7.24983879766308));
#17370=CARTESIAN_POINT('Ctrl Pts',(-1.76250564706505,2.73752337116124,-7.09091692266307));
#17371=CARTESIAN_POINT('Ctrl Pts',(-3.25276476936475,0.000797871361256092,
-6.93199504766308));
#17372=CARTESIAN_POINT('Ctrl Pts',(-1.76373954051992,-2.73410913803656,
-6.77307317266308));
#17373=CARTESIAN_POINT('Ctrl Pts',(1.34420947621469,-2.96334697858288,-6.61415129766307));
#17374=CARTESIAN_POINT('Ctrl Pts',(3.21872665857139,-0.474706893552386,
-6.45522942266308));
#17375=CARTESIAN_POINT('Ctrl Pts',(2.14235137112462,2.44884671975765,-6.29630754766308));
#17376=CARTESIAN_POINT('Ctrl Pts',(-0.898655362480478,3.12716261166621,
-6.13738567266308));
#17377=CARTESIAN_POINT('Ctrl Pts',(-3.11553039135719,0.937984586728336,
-5.97846379766308));
#17378=CARTESIAN_POINT('Ctrl Pts',(-2.4757415385533,-2.11121017092211,-5.81954192266308));
#17379=CARTESIAN_POINT('Ctrl Pts',(0.434168366430812,-3.2245955396039,-5.66062004766308));
#17380=CARTESIAN_POINT('Ctrl Pts',(2.94595745262798,-1.38123195041602,-5.50169817266308));
#17381=CARTESIAN_POINT('Ctrl Pts',(2.75651315946459,1.728620131259,-5.34277629766308));
#17382=CARTESIAN_POINT('Ctrl Pts',(0.0395287622217419,3.25344887201774,
-5.18385442266308));
#17383=CARTESIAN_POINT('Ctrl Pts',(-2.71369826611098,1.79508413267342,-5.02493254766308));
#17384=CARTESIAN_POINT('Ctrl Pts',(-2.97864976828788,-1.3092497015674,-4.86601067266307));
#17385=CARTESIAN_POINT('Ctrl Pts',(-0.512381191680485,-3.21309109372021,
-4.70708879766308));
#17386=CARTESIAN_POINT('Ctrl Pts',(2.42370574697401,-2.17074605928956,-4.54816692266308));
#17387=CARTESIAN_POINT('Ctrl Pts',(3.13741944356645,0.862025418568423,-4.38924504766307));
#17388=CARTESIAN_POINT('Ctrl Pts',(0.974332658922546,3.104378256774,-4.23032317266308));
#17389=CARTESIAN_POINT('Ctrl Pts',(-2.08215089725633,2.50022719478358,-4.07140129766307));
#17390=CARTESIAN_POINT('Ctrl Pts',(-3.2294436301607,-0.396462244353565,
-3.91247942266308));
#17391=CARTESIAN_POINT('Ctrl Pts',(-1.41555604262275,-2.92962276506217,
-3.75355754766307));
#17392=CARTESIAN_POINT('Ctrl Pts',(1.69630021382975,-2.7765183261488,-3.59463567266308));
#17393=CARTESIAN_POINT('Ctrl Pts',(3.25276447524416,-0.0775353078662964,
-3.43571379766308));
#17394=CARTESIAN_POINT('Ctrl Pts',(1.82666479701668,2.69254232852956,-3.27679192266308));
#17395=CARTESIAN_POINT('Ctrl Pts',(-1.27436233859685,2.99374164123204,-3.11787004766308));
#17396=CARTESIAN_POINT('Ctrl Pts',(-3.20688583420982,0.549883385563377,
-2.95894817266308));
#17397=CARTESIAN_POINT('Ctrl Pts',(-2.19891297674939,-2.39818062451726,
-2.80002629766308));
#17398=CARTESIAN_POINT('Ctrl Pts',(0.825313597989087,-3.14727588031465,
-2.64110442266308));
#17399=CARTESIAN_POINT('Ctrl Pts',(3.09278374493772,-1.01053330928825,-2.48218254766308));
#17400=CARTESIAN_POINT('Ctrl Pts',(2.52438132473606,2.05280007562831,-2.32326067266307));
#17401=CARTESIAN_POINT('Ctrl Pts',(-0.358707023041385,3.23385444856295,
-2.16433879766308));
#17402=CARTESIAN_POINT('Ctrl Pts',(-2.91288573121381,1.44968576000706,-2.00541692266308));
#17403=CARTESIAN_POINT('Ctrl Pts',(-2.79614559896779,-1.66374942400242,
-1.84649504766308));
#17404=CARTESIAN_POINT('Ctrl Pts',(-0.11553117501689,-3.25163336819261,
-1.68757317266307));
#17405=CARTESIAN_POINT('Ctrl Pts',(2.67101972474585,-1.858002205182,-1.52865129766308));
#17406=CARTESIAN_POINT('Ctrl Pts',(3.00842279450199,1.23931305207524,-1.36972942266307));
#17407=CARTESIAN_POINT('Ctrl Pts',(0.587314853311628,3.20021967488011,-1.21080754766308));
#17408=CARTESIAN_POINT('Ctrl Pts',(-2.37233660763231,2.22682430389234,-1.05188567266308));
#17409=CARTESIAN_POINT('Ctrl Pts',(-3.15668655600379,-0.7885744361646,-0.892963797663079));
#17410=CARTESIAN_POINT('Ctrl Pts',(-1.04662708835568,-3.08060378421251,
-0.734041922663075));
#17411=CARTESIAN_POINT('Ctrl Pts',(2.02322853672912,-2.54850362361652,-0.575120047663078));
#17412=CARTESIAN_POINT('Ctrl Pts',(3.23771006659529,0.321501897593122,-0.416198172663076));
#17413=CARTESIAN_POINT('Ctrl Pts',(1.48383540713939,2.89460045013793,-0.257276297663075));
#17414=CARTESIAN_POINT('Ctrl Pts',(-1.63138756367065,2.81762931924888,-0.0983544226630758));
#17415=CARTESIAN_POINT('Ctrl Pts',(-3.24926952928756,0.148909660017409,
0.0605674523369241));
#17416=CARTESIAN_POINT('Ctrl Pts',(-2.34351741732464,-1.70878854385852,
0.166515369003591));
#17417=CARTESIAN_POINT('Ctrl Pts',(-1.59774743137966,-2.24059110187412,
0.219489327336924));
#17418=CARTESIAN_POINT('Ctrl Pts',(2.91090525077879,0.426608275808731,-7.29901600899462));
#17419=CARTESIAN_POINT('Ctrl Pts',(2.7689107353191,1.39548910647197,-7.24604205066128));
#17420=CARTESIAN_POINT('Ctrl Pts',(1.44373367001803,3.16348122238413,-7.14009413399461));
#17421=CARTESIAN_POINT('Ctrl Pts',(-1.88424732350133,2.9266125153825,-6.98117225899462));
#17422=CARTESIAN_POINT('Ctrl Pts',(-3.47744321889753,0.000852982785874625,
-6.82225038399461));
#17423=CARTESIAN_POINT('Ctrl Pts',(-1.88556644576554,-2.92296245069324,
-6.66332850899462));
#17424=CARTESIAN_POINT('Ctrl Pts',(1.43705815184215,-3.16803445271144,-6.50440663399462));
#17425=CARTESIAN_POINT('Ctrl Pts',(3.441053991285,-0.507496356175199,-6.3454847589946));
#17426=CARTESIAN_POINT('Ctrl Pts',(2.29033015795609,2.61799608134706,-6.18656288399462));
#17427=CARTESIAN_POINT('Ctrl Pts',(-0.960728247494492,3.34316533453242,
-6.02764100899461));
#17428=CARTESIAN_POINT('Ctrl Pts',(-3.33072964105243,1.00277406201306,-5.86871913399463));
#17429=CARTESIAN_POINT('Ctrl Pts',(-2.64674860785167,-2.25703793944323,
-5.7097972589946));
#17430=CARTESIAN_POINT('Ctrl Pts',(0.464157708520523,-3.44732825394955,
-5.55087538399462));
#17431=CARTESIAN_POINT('Ctrl Pts',(3.14944377880805,-1.4766378820061,-5.39195350899461));
#17432=CARTESIAN_POINT('Ctrl Pts',(2.94691398666802,1.84802123108039,-5.23303163399462));
#17433=CARTESIAN_POINT('Ctrl Pts',(0.0422591351929435,3.47817457462115,
-5.07410975899461));
#17434=CARTESIAN_POINT('Ctrl Pts',(-2.90114173717657,1.91907610513589,-4.91518788399462));
#17435=CARTESIAN_POINT('Ctrl Pts',(-3.18439425308528,-1.39968359822352,
-4.75626600899461));
#17436=CARTESIAN_POINT('Ctrl Pts',(-0.547772933745816,-3.43502916066676,
-4.59734413399462));
#17437=CARTESIAN_POINT('Ctrl Pts',(2.59111854438333,-2.32068615441235,-4.43842225899462));
#17438=CARTESIAN_POINT('Ctrl Pts',(3.35413063730339,0.921568160892088,-4.27950038399461));
#17439=CARTESIAN_POINT('Ctrl Pts',(1.04163280715265,3.31880719429335,-4.12057850899462));
#17440=CARTESIAN_POINT('Ctrl Pts',(-2.22597145252513,2.67292556353571,-3.96165663399461));
#17441=CARTESIAN_POINT('Ctrl Pts',(-3.45251121700612,-0.423847108822882,
-3.80273475899462));
#17442=CARTESIAN_POINT('Ctrl Pts',(-1.51333284464627,-3.13198080421993,
-3.64381288399462));
#17443=CARTESIAN_POINT('Ctrl Pts',(1.81346887772297,-2.96830097163666,-3.48489100899461));
#17444=CARTESIAN_POINT('Ctrl Pts',(3.47744290446113,-0.0828909096360698,
-3.32596913399462));
#17445=CARTESIAN_POINT('Ctrl Pts',(1.95283814292696,2.87852449403166,-3.16704725899461));
#17446=CARTESIAN_POINT('Ctrl Pts',(-1.36238645797847,3.20052856803004,-3.00812538399462));
#17447=CARTESIAN_POINT('Ctrl Pts',(-3.42839528483007,0.587865519302596,
-2.84920350899461));
#17448=CARTESIAN_POINT('Ctrl Pts',(-2.35079864734157,-2.5638303233491,-2.69028163399462));
#17449=CARTESIAN_POINT('Ctrl Pts',(0.882320542149611,-3.36466788839986,
-2.53135975899461));
#17450=CARTESIAN_POINT('Ctrl Pts',(3.30641181392608,-1.0803339475854,-2.37243788399462));
#17451=CARTESIAN_POINT('Ctrl Pts',(2.69874809340406,2.19459327953189,-2.21351600899462));
#17452=CARTESIAN_POINT('Ctrl Pts',(-0.383484018455407,3.45722670417789,
-2.05459413399462));
#17453=CARTESIAN_POINT('Ctrl Pts',(-3.11408769205621,1.54982000639825,-1.89567225899462));
#17454=CARTESIAN_POINT('Ctrl Pts',(-2.98928396045057,-1.77866970490208,
-1.73675038399462));
#17455=CARTESIAN_POINT('Ctrl Pts',(-0.123511267988871,-3.47623366837271,
-1.57782850899461));
#17456=CARTESIAN_POINT('Ctrl Pts',(2.8555152579241,-1.98634012208901,-1.41890663399462));
#17457=CARTESIAN_POINT('Ctrl Pts',(3.21622379363166,1.32491620962554,-1.25998475899462));
#17458=CARTESIAN_POINT('Ctrl Pts',(0.627882493453467,3.42126867340845,-1.10106288399462));
#17459=CARTESIAN_POINT('Ctrl Pts',(-2.53620118086942,2.38063789554599,-0.942141008994616));
#17460=CARTESIAN_POINT('Ctrl Pts',(-3.3747285883523,-0.843043693618233,
-0.783219133994615));
#17461=CARTESIAN_POINT('Ctrl Pts',(-1.11892083479118,-3.29339054591764,
-0.624297258994616));
#17462=CARTESIAN_POINT('Ctrl Pts',(2.1629791436479,-2.72453659353051,-0.465375383994615));
#17463=CARTESIAN_POINT('Ctrl Pts',(3.46134864158557,0.343709020762119,-0.306453508994615));
#17464=CARTESIAN_POINT('Ctrl Pts',(1.58632847450714,3.0945393904754,-0.147531633994614));
#17465=CARTESIAN_POINT('Ctrl Pts',(-1.74407251151708,3.0122516272526,0.0113902410053857));
#17466=CARTESIAN_POINT('Ctrl Pts',(-3.47370655185682,0.159195307429815,
0.170312116005385));
#17467=CARTESIAN_POINT('Ctrl Pts',(-2.5053913606041,-1.82681981504955,0.276260032672052));
#17468=CARTESIAN_POINT('Ctrl Pts',(-1.70810875200399,-2.39535560853235,
0.329233991005385));
#17469=CARTESIAN_POINT('Ctrl Pts',(2.34668236863854,0.343918483395443,-7.62825));
#17470=CARTESIAN_POINT('Ctrl Pts',(2.23221075339669,1.12500043789087,-7.57527604166667));
#17471=CARTESIAN_POINT('Ctrl Pts',(1.16389372259185,2.55030135594479,-7.469328125));
#17472=CARTESIAN_POINT('Ctrl Pts',(-1.5190222941925,2.35934508271871,-7.31040625));
#17473=CARTESIAN_POINT('Ctrl Pts',(-2.37547941669845,0.786539379620308,
-7.20443357769833));
#17474=CARTESIAN_POINT('Ctrl Pts',(-2.37545665643198,0.00021427761423283,
-7.15143486372999));
#17475=CARTESIAN_POINT('Ctrl Pts',(-2.37545655236239,-0.000153013793341093,
-7.15141010809498));
#17476=CARTESIAN_POINT('Ctrl Pts',(-1.29202279186848,2.64852742499071,1.38777878078145E-15));
#17477=CARTESIAN_POINT('Ctrl Pts',(-1.35199458296097,2.61237463056833,1.3768917757166E-15));
#17478=CARTESIAN_POINT('Ctrl Pts',(-1.41049170787627,2.57398608239727,1.45861512784923E-15));
#17479=CARTESIAN_POINT('Ctrl Pts',(-1.4673716833267,2.53335400329109,3.88578058618805E-16));
#17480=CARTESIAN_POINT('Ctrl Pts',(-1.54687248640264,2.47656278821044,-1.16360444155571E-15));
#17481=CARTESIAN_POINT('Ctrl Pts',(-1.62321595271307,2.41538961241442,-1.82659121223932E-15));
#17482=CARTESIAN_POINT('Ctrl Pts',(-1.69622598732601,2.35021369122793,-1.94289029309402E-15));
#17483=CARTESIAN_POINT('Ctrl Pts',(-1.73503288464287,2.31557084665972,-2.00470654222609E-15));
#17484=CARTESIAN_POINT('Ctrl Pts',(-1.77289731557515,2.27979657283835,-3.6596624852132E-15));
#17485=CARTESIAN_POINT('Ctrl Pts',(-1.80978776603342,2.24294480419717,-4.27435864480685E-15));
#17486=CARTESIAN_POINT('Ctrl Pts',(-1.82764687861092,2.22510441795447,-4.5719404790963E-15));
#17487=CARTESIAN_POINT('Ctrl Pts',(-1.84527766969911,2.207011480151,-6.28754868127402E-15));
#17488=CARTESIAN_POINT('Ctrl Pts',(-1.86267624534788,2.18867199094149,-6.60582699651968E-15));
#17489=CARTESIAN_POINT('Ctrl Pts',(-1.87902498126204,2.17143911671434,-6.9049002211444E-15));
#17490=CARTESIAN_POINT('Ctrl Pts',(-1.8951717260503,2.15398497639697,-1.91704975695889E-15));
#17491=CARTESIAN_POINT('Ctrl Pts',(-1.91109358900524,2.13633667768233,-2.1094237467878E-15));
#17492=CARTESIAN_POINT('Ctrl Pts',(-1.9762348782431,2.06413200324311,-2.89648552145286E-15));
#17493=CARTESIAN_POINT('Ctrl Pts',(-2.03767664102131,1.98861789173561,-5.92176889494793E-15));
#17494=CARTESIAN_POINT('Ctrl Pts',(-2.09524485736161,1.91016955933988,-4.9960036108132E-15));
#17495=CARTESIAN_POINT('Ctrl Pts',(-2.14241512558355,1.84589053323986,-4.23744968054974E-15));
#17496=CARTESIAN_POINT('Ctrl Pts',(-2.1869840436588,1.77964066924168,-3.01258662690371E-15));
#17497=CARTESIAN_POINT('Ctrl Pts',(-2.22883162278026,1.71161678957997,-3.05311331771918E-15));
#17498=CARTESIAN_POINT('Ctrl Pts',(-2.24785166956067,1.68069941274449,-3.07153301059863E-15));
#17499=CARTESIAN_POINT('Ctrl Pts',(-2.26630923741872,1.64941548477482,-1.8357015969624E-15));
#17500=CARTESIAN_POINT('Ctrl Pts',(-2.28419144786431,1.61778322747023,-1.97064586870965E-15));
#17501=CARTESIAN_POINT('Ctrl Pts',(-2.2947105199583,1.5991757965771,-2.05002579366356E-15));
#17502=CARTESIAN_POINT('Ctrl Pts',(-2.30503048226771,1.58044783181963,-2.22291906330319E-15));
#17503=CARTESIAN_POINT('Ctrl Pts',(-2.315148542904,1.56160303675851,-2.13717932240343E-15));
#17504=CARTESIAN_POINT('Ctrl Pts',(-2.32240461406201,1.54808867083041,-2.07569188094589E-15));
#17505=CARTESIAN_POINT('Ctrl Pts',(-2.32955662819893,1.53451447386006,-2.90245848901719E-15));
#17506=CARTESIAN_POINT('Ctrl Pts',(-2.3365973589752,1.52089422682565,-2.88657986402541E-15));
#17507=CARTESIAN_POINT('Ctrl Pts',(-2.38026140223708,1.43642642445602,-2.78810642559811E-15));
#17508=CARTESIAN_POINT('Ctrl Pts',(-2.41971487734872,1.35006846525182,-1.99369284366072E-15));
#17509=CARTESIAN_POINT('Ctrl Pts',(-2.45479279162088,1.26216638421689,-1.97064586870965E-15));
#17510=CARTESIAN_POINT('Ctrl Pts',(-2.49091088104935,1.17165771830431,-1.94691547539493E-15));
#17511=CARTESIAN_POINT('Ctrl Pts',(-2.52239067717506,1.07951100453385,-3.03582794683908E-15));
#17512=CARTESIAN_POINT('Ctrl Pts',(-2.54899471108211,0.986093738756397,
-3.46944695195361E-15));
#17513=CARTESIAN_POINT('Ctrl Pts',(-2.5737480130153,0.899175123570395,-3.87290088661142E-15));
#17514=CARTESIAN_POINT('Ctrl Pts',(-2.59427998939988,0.811155810374791,
-6.26468692693552E-16));
#17515=CARTESIAN_POINT('Ctrl Pts',(-2.61035012881561,0.722335842771595,
-3.05311331771918E-16));
#17516=CARTESIAN_POINT('Ctrl Pts',(-2.6194911252636,0.671813380746323,-1.22631006512308E-16));
#17517=CARTESIAN_POINT('Ctrl Pts',(-2.62718758589052,0.621031999246336,
-2.43292193953287E-15));
#17518=CARTESIAN_POINT('Ctrl Pts',(-2.63338792296817,0.570048893516924,
-2.4980018054066E-15));
#17519=CARTESIAN_POINT('Ctrl Pts',(-2.63582396293746,0.550018227157934,
-2.5235709240657E-15));
#17520=CARTESIAN_POINT('Ctrl Pts',(-2.63802946464811,0.52995046931884,-1.18365939012317E-16));
#17521=CARTESIAN_POINT('Ctrl Pts',(-2.63999815788099,0.509882529321155,
-2.4980018054066E-16));
#17522=CARTESIAN_POINT('Ctrl Pts',(-2.64870462915334,0.421132824610296,
-8.31063136573107E-16));
#17523=CARTESIAN_POINT('Ctrl Pts',(-2.65279857511044,0.332278776698517,
-1.41266709339503E-15));
#17524=CARTESIAN_POINT('Ctrl Pts',(-2.65209667942641,0.24361098136173,-1.2490009027033E-15));
#17525=CARTESIAN_POINT('Ctrl Pts',(-2.65178160418319,0.20380873179956,-1.17553248565223E-15));
#17526=CARTESIAN_POINT('Ctrl Pts',(-2.65049946631159,0.164044057031022,
-2.27209153104153E-15));
#17527=CARTESIAN_POINT('Ctrl Pts',(-2.64823027091117,0.124343747519916,
-2.05391259555654E-15));
#17528=CARTESIAN_POINT('Ctrl Pts',(-2.64306952052804,0.0340547457521929,
-1.55872864938796E-15));
#17529=CARTESIAN_POINT('Ctrl Pts',(-2.63280652105649,-0.0559028803342746,
-7.21832289429463E-16));
#17530=CARTESIAN_POINT('Ctrl Pts',(-2.61763767596916,-0.145196339325471,
-5.55111512312578E-17));
#17531=CARTESIAN_POINT('Ctrl Pts',(-2.60203111097934,-0.237066495747391,
6.30037688348759E-16));
#17532=CARTESIAN_POINT('Ctrl Pts',(-2.58123101177304,-0.32823466497094,
1.60028609533083E-17));
#17533=CARTESIAN_POINT('Ctrl Pts',(-2.55540429049513,-0.418306656786799,
-2.77555756156289E-17));
#17534=CARTESIAN_POINT('Ctrl Pts',(-2.55124208238436,-0.432822567298845,
-3.48076407090747E-17));
#17535=CARTESIAN_POINT('Ctrl Pts',(-2.5469492344459,-0.447309922326401,
2.38273081097328E-16));
#17536=CARTESIAN_POINT('Ctrl Pts',(-2.5425263488523,-0.461766968021027,
2.35922392732846E-16));
#17537=CARTESIAN_POINT('Ctrl Pts',(-2.53834316813649,-0.475440492573617,
2.33699103428367E-16));
#17538=CARTESIAN_POINT('Ctrl Pts',(-2.53404591398863,-0.489079439047373,
-2.93330448010983E-15));
#17539=CARTESIAN_POINT('Ctrl Pts',(-2.5296372776324,-0.502677071255232,
-2.85882428840978E-15));
#17540=CARTESIAN_POINT('Ctrl Pts',(-2.50226678515391,-0.587096347420926,
-2.39642291029584E-15));
#17541=CARTESIAN_POINT('Ctrl Pts',(-2.47058652949289,-0.66999248339392,
8.43465801160117E-16));
#17542=CARTESIAN_POINT('Ctrl Pts',(-2.43480876844775,-0.751061931359657,
4.57966997657877E-16));
#17543=CARTESIAN_POINT('Ctrl Pts',(-2.39908751409446,-0.832003339834344,
7.30770433810818E-17));
#17544=CARTESIAN_POINT('Ctrl Pts',(-2.35928102567076,-0.911124606962677,
-4.15813315017429E-16));
#17545=CARTESIAN_POINT('Ctrl Pts',(-2.31555847154045,-0.988093622425155,
-6.24500451351651E-16));
#17546=CARTESIAN_POINT('Ctrl Pts',(-2.27253682415144,-1.06382876436671,
-8.29842169661056E-16));
#17547=CARTESIAN_POINT('Ctrl Pts',(-2.22572298419624,-1.13748072263154,
8.17918205727042E-18));
#17548=CARTESIAN_POINT('Ctrl Pts',(-2.17524736269965,-1.20869383031328,
-2.77555756156289E-16));
#17549=CARTESIAN_POINT('Ctrl Pts',(-2.15801966745604,-1.2329993798066,-3.75079160327306E-16));
#17550=CARTESIAN_POINT('Ctrl Pts',(-2.14036518691089,-1.25702044358516,
-4.12077394156608E-16));
#17551=CARTESIAN_POINT('Ctrl Pts',(-2.12228847798412,-1.28074161564621,
-3.33066907387547E-16));
#17552=CARTESIAN_POINT('Ctrl Pts',(-2.1108121718594,-1.29580140519709,-2.82905755991096E-16));
#17553=CARTESIAN_POINT('Ctrl Pts',(-2.09916567817787,-1.31074030793348,
-5.65747126062716E-16));
#17554=CARTESIAN_POINT('Ctrl Pts',(-2.08735010827511,-1.3255542322009,-6.31439345255558E-16));
#17555=CARTESIAN_POINT('Ctrl Pts',(-2.07893549744778,-1.33610415984397,
-6.78222908252514E-16));
#17556=CARTESIAN_POINT('Ctrl Pts',(-2.0704406728309,-1.34658373111037,1.09442983389869E-15));
#17557=CARTESIAN_POINT('Ctrl Pts',(-2.06186814397016,-1.35698959226187,
1.03389519168218E-15));
#17558=CARTESIAN_POINT('Ctrl Pts',(-2.0076512765473,-1.42280135021988,6.51044492097758E-16));
#17559=CARTESIAN_POINT('Ctrl Pts',(-1.95030545375966,-1.48569742630702,
-3.12596990479738E-15));
#17560=CARTESIAN_POINT('Ctrl Pts',(-1.88998858415622,-1.54538141434951,
-2.46330733588707E-15));
#17561=CARTESIAN_POINT('Ctrl Pts',(-1.8306216693761,-1.60412541507686,-1.81108130832433E-15));
#17562=CARTESIAN_POINT('Ctrl Pts',(-1.76837591722446,-1.65975822361316,
8.06391941282204E-16));
#17563=CARTESIAN_POINT('Ctrl Pts',(-1.70337601327298,-1.71195478590349,
7.07767178198537E-16));
#17564=CARTESIAN_POINT('Ctrl Pts',(-1.64040340588573,-1.76252337792058,
6.12218444942487E-16));
#17565=CARTESIAN_POINT('Ctrl Pts',(-1.57484520000723,-1.8098670152844,2.93571211404161E-16));
#17566=CARTESIAN_POINT('Ctrl Pts',(-1.50679910444526,-1.85364436762269,
4.66640615037761E-16));
#17567=CARTESIAN_POINT('Ctrl Pts',(-1.46449561434321,-1.88086025379576,
5.7423591118395E-16));
#17568=CARTESIAN_POINT('Ctrl Pts',(-1.42123028569669,-1.90669686113838,
1.15169204501483E-15));
#17569=CARTESIAN_POINT('Ctrl Pts',(-1.37702479013101,-1.93106208855766,
1.11022302462516E-15));
#17570=CARTESIAN_POINT('Origin',(0.,0.,-9.84858989190502));
#17571=CARTESIAN_POINT('Origin',(0.,0.,24.));
#17572=CARTESIAN_POINT('',(-6.,-7.34788079488412E-16,24.));
#17573=CARTESIAN_POINT('Origin',(0.,0.,24.));
#17574=CARTESIAN_POINT('',(-4.,-4.89858719658941E-16,24.));
#17575=CARTESIAN_POINT('Origin',(0.,0.,24.));
#17576=CARTESIAN_POINT('Origin',(0.,0.,24.));
#17577=CARTESIAN_POINT('',(-6.,-7.34788079488412E-16,28.));
#17578=CARTESIAN_POINT('Origin',(0.,0.,28.));
#17579=CARTESIAN_POINT('',(-6.,-7.34788079488412E-16,24.));
#17580=CARTESIAN_POINT('Origin',(0.,0.,28.));
#17581=CARTESIAN_POINT('Origin',(0.,0.,0.));
#17582=CARTESIAN_POINT('',(-4.,-4.89858719658941E-16,0.));
#17583=CARTESIAN_POINT('Origin',(0.,0.,0.));
#17584=CARTESIAN_POINT('Origin',(0.,0.,0.));
#17585=CARTESIAN_POINT('',(-4.,-4.89858719658941E-16,0.));
#17586=CARTESIAN_POINT('Origin',(0.,0.,-8.));
#19840=UNCERTAINTY_MEASURE_WITH_UNIT(LENGTH_MEASURE(0.01),#19864,
'DISTANCE_ACCURACY_VALUE',
'Maximum model space distance between geometric entities at asserted c
onnectivities');
#19842=UNCERTAINTY_MEASURE_WITH_UNIT(LENGTH_MEASURE(0.01),#19864,
'DISTANCE_ACCURACY_VALUE',
'Maximum model space distance between geometric entities at asserted c
onnectivities');
#19861=(
GEOMETRIC_REPRESENTATION_CONTEXT(3)
GLOBAL_UNCERTAINTY_ASSIGNED_CONTEXT((#19840))
GLOBAL_UNIT_ASSIGNED_CONTEXT((#19864,#19866,#19867))
REPRESENTATION_CONTEXT('','3D')
);
#19863=(
GEOMETRIC_REPRESENTATION_CONTEXT(3)
GLOBAL_UNCERTAINTY_ASSIGNED_CONTEXT((#19842))
GLOBAL_UNIT_ASSIGNED_CONTEXT((#19864,#19866,#19867))
REPRESENTATION_CONTEXT('','3D')
);
#19864=(
LENGTH_UNIT()
NAMED_UNIT(*)
SI_UNIT(.MILLI.,.METRE.)
);
#19866=(
NAMED_UNIT(*)
PLANE_ANGLE_UNIT()
SI_UNIT($,.RADIAN.)
);
#19867=(
NAMED_UNIT(*)
SI_UNIT($,.STERADIAN.)
SOLID_ANGLE_UNIT()
);
#19886=SHAPE_DEFINITION_REPRESENTATION(#19906,#19952);
#19906=PRODUCT_DEFINITION_SHAPE('',$,#19973);
#19952=SHAPE_REPRESENTATION('',(#7076),#19861);
#19954=PRODUCT_DEFINITION_CONTEXT('part definition',#20016,'design');
#19973=PRODUCT_DEFINITION('Shoulder screw M6x8','Shoulder screw M6x8',#19993,
#19954);
#19993=PRODUCT_DEFINITION_FORMATION('',$,#20036);
#20016=APPLICATION_CONTEXT(
'Core Data for Automotive Mechanical Design Process');
#20017=PRODUCT_CONTEXT('part definition',#20016,'mechanical');
#20036=PRODUCT('Shoulder screw M6x8','Shoulder screw M6x8',$,(#20017));
#20042=PRESENTATION_STYLE_ASSIGNMENT((#20049));
#20049=SURFACE_STYLE_USAGE(.BOTH.,#20056);
#20056=SURFACE_SIDE_STYLE('',(#20063));
#20063=SURFACE_STYLE_FILL_AREA(#20070);
#20070=FILL_AREA_STYLE('Gray',(#20077));
#20077=FILL_AREA_STYLE_COLOUR('Gray',#20084);
#20084=COLOUR_RGB('Gray',0.407843137254902,0.447058823529412,0.498039215686275);
ENDSEC;
END-ISO-10303-21;
